ISO-10303-21;
HEADER;
FILE_DESCRIPTION (('STEP AP214'),
    '1' );
FILE_NAME ('Outlet Housing.step',
    '2026-10-23T18:01:19',
    ( '' ),
    ( '' ),
    'SwSTEP 2.0',
    'SolidWorks 2025',
    '' );
FILE_SCHEMA (( 'AUTOMOTIVE_DESIGN' ));
ENDSEC;

DATA;
#4=DIRECTION ( 'NONE',  ( 0.000000000000000000, 0.000000000000000000, -1.000000000000000000 ) ) ;
#7=CYLINDRICAL_SURFACE ( 'NONE', #13072, 0.7849999999999998090 ) ;
#12=CARTESIAN_POINT ( 'NONE',  ( 2.742999999999999883, -1.679378605318041950, 1.679378605318059048 ) ) ;
#13=ADVANCED_FACE ( 'NONE', ( #4673 ), #12779, .T. ) ;
#16=AXIS2_PLACEMENT_3D ( 'NONE', #9213, #3471, #11656 ) ;
#17=CARTESIAN_POINT ( 'NONE',  ( 2.124999999999999556, 2.359999999999994547, -1.575000000000016831 ) ) ;
#30=CARTESIAN_POINT ( 'NONE',  ( 2.774999999999999911, -0.9799999999999436939, 2.360000000000016307 ) ) ;
#31=DIRECTION ( 'NONE',  ( -1.000000000000000000, -0.000000000000000000, -0.000000000000000000 ) ) ;
#37=ORIENTED_EDGE ( 'NONE', *, *, #11617, .T. ) ;
#38=CARTESIAN_POINT ( 'NONE',  ( 2.774999999999999911, -2.360000000000000320, 0.9799999999999999822 ) ) ;
#40=ADVANCED_FACE ( 'NONE', ( #12760 ), #3290, .F. ) ;
#46=EDGE_CURVE ( 'NONE', #11318, #5162, #12173, .T. ) ;
#53=CARTESIAN_POINT ( 'NONE',  ( 2.742999999999999883, -1.679378605318041950, 1.941878605318059003 ) ) ;
#55=DIRECTION ( 'NONE',  ( -1.000000000000000000, -0.000000000000000000, 0.000000000000000000 ) ) ;
#56=CARTESIAN_POINT ( 'NONE',  ( 1.375000000000000000, 1.653273178848927113E-16, -1.350000000000000089 ) ) ;
#59=AXIS2_PLACEMENT_3D ( 'NONE', #1494, #12413, #11192 ) ;
#62=ORIENTED_EDGE ( 'NONE', *, *, #9280, .T. ) ;
#67=FACE_OUTER_BOUND ( 'NONE', #2223, .T. ) ;
#71=ADVANCED_FACE ( 'NONE', ( #976 ), #2655, .T. ) ;
#75=CARTESIAN_POINT ( 'NONE',  ( 2.774999999999999911, 1.679378605318042395, -1.679378605318058604 ) ) ;
#77=ORIENTED_EDGE ( 'NONE', *, *, #5878, .F. ) ;
#82=ORIENTED_EDGE ( 'NONE', *, *, #11617, .F. ) ;
#85=FACE_OUTER_BOUND ( 'NONE', #9329, .T. ) ;
#87=DIRECTION ( 'NONE',  ( -1.000000000000000000, -0.000000000000000000, -0.000000000000000000 ) ) ;
#88=EDGE_CURVE ( 'NONE', #13385, #4765, #4744, .T. ) ;
#91=ORIENTED_EDGE ( 'NONE', *, *, #3376, .F. ) ;
#92=FACE_BOUND ( 'NONE', #13262, .T. ) ;
#109=DIRECTION ( 'NONE',  ( 0.000000000000000000, 0.000000000000000000, -1.000000000000000000 ) ) ;
#112=ORIENTED_EDGE ( 'NONE', *, *, #14877, .T. ) ;
#118=ORIENTED_EDGE ( 'NONE', *, *, #160, .F. ) ;
#120=CARTESIAN_POINT ( 'NONE',  ( 2.061999999999999389, 0.000000000000000000, 0.000000000000000000 ) ) ;
#125=ADVANCED_FACE ( 'NONE', ( #8119 ), #11202, .T. ) ;
#126=DIRECTION ( 'NONE',  ( 0.000000000000000000, 0.000000000000000000, 1.000000000000000000 ) ) ;
#127=CARTESIAN_POINT ( 'NONE',  ( 2.124999999999999556, -0.6999999999999598765, 2.400000000000012346 ) ) ;
#130=ORIENTED_EDGE ( 'NONE', *, *, #6487, .T. ) ;
#131=CARTESIAN_POINT ( 'NONE',  ( 2.774999999999999911, 2.360000000000015863, 1.574999999999999956 ) ) ;
#132=CARTESIAN_POINT ( 'NONE',  ( 0.000000000000000000, 0.000000000000000000, 0.000000000000000000 ) ) ;
#133=EDGE_LOOP ( 'NONE', ( #9480, #11934, #9524, #6761 ) ) ;
#135=CIRCLE ( 'NONE', #14993, 0.7849999999999993650 ) ;
#136=FACE_OUTER_BOUND ( 'NONE', #12337, .T. ) ;
#137=ADVANCED_FACE ( 'NONE', ( #6971 ), #13149, .T. ) ;
#141=CARTESIAN_POINT ( 'NONE',  ( 2.124999999999999556, -1.679378605318041950, 1.973878605318058810 ) ) ;
#142=CIRCLE ( 'NONE', #9202, 0.3750000000000007772 ) ;
#144=EDGE_CURVE ( 'NONE', #5162, #1223, #2289, .T. ) ;
#151=DIRECTION ( 'NONE',  ( -1.000000000000000000, -0.000000000000000000, -0.000000000000000000 ) ) ;
#152=EDGE_LOOP ( 'NONE', ( #2875, #13382, #6419, #11719 ) ) ;
#153=CYLINDRICAL_SURFACE ( 'NONE', #7144, 1.000000000000000444 ) ;
#157=CIRCLE ( 'NONE', #12372, 0.05999999999999990757 ) ;
#160=EDGE_CURVE ( 'NONE', #1104, #11415, #8533, .T. ) ;
#167=VERTEX_POINT ( 'NONE', #2214 ) ;
#169=AXIS2_PLACEMENT_3D ( 'NONE', #3610, #8290, #3527 ) ;
#171=EDGE_CURVE ( 'NONE', #13385, #5675, #9017, .T. ) ;
#180=ADVANCED_FACE ( 'NONE', ( #3680 ), #7071, .F. ) ;
#183=VECTOR ( 'NONE', #7595, 39.37007874015748143 ) ;
#185=CARTESIAN_POINT ( 'NONE',  ( 2.774999999999999911, 0.000000000000000000, 0.000000000000000000 ) ) ;
#186=EDGE_LOOP ( 'NONE', ( #11801, #8509, #1158, #8869 ) ) ;
#188=DIRECTION ( 'NONE',  ( 1.000000000000000000, 0.000000000000000000, 0.000000000000000000 ) ) ;
#193=VERTEX_POINT ( 'NONE', #1581 ) ;
#198=EDGE_CURVE ( 'NONE', #9755, #1223, #6326, .T. ) ;
#208=AXIS2_PLACEMENT_3D ( 'NONE', #5410, #13799, #3334 ) ;
#212=ORIENTED_EDGE ( 'NONE', *, *, #11674, .T. ) ;
#214=FACE_OUTER_BOUND ( 'NONE', #11433, .T. ) ;
#216=DIRECTION ( 'NONE',  ( 1.000000000000000000, 0.000000000000000000, 0.000000000000000000 ) ) ;
#222=AXIS2_PLACEMENT_3D ( 'NONE', #2084, #6691, #5471 ) ;
#225=LINE ( 'NONE', #9876, #6827 ) ;
#229=DIRECTION ( 'NONE',  ( 0.7071067811865474617, 8.659560562354932858E-17, 0.7071067811865474617 ) ) ;
#232=ORIENTED_EDGE ( 'NONE', *, *, #13602, .F. ) ;
#233=EDGE_CURVE ( 'NONE', #5394, #8971, #13378, .T. ) ;
#237=LINE ( 'NONE', #14244, #10985 ) ;
#242=LINE ( 'NONE', #7239, #4272 ) ;
#245=ORIENTED_EDGE ( 'NONE', *, *, #2104, .F. ) ;
#248=FACE_OUTER_BOUND ( 'NONE', #14126, .T. ) ;
#261=VERTEX_POINT ( 'NONE', #9572 ) ;
#266=ORIENTED_EDGE ( 'NONE', *, *, #8038, .T. ) ;
#277=EDGE_CURVE ( 'NONE', #13668, #9005, #9364, .T. ) ;
#283=ORIENTED_EDGE ( 'NONE', *, *, #1026, .F. ) ;
#285=( NAMED_UNIT ( * ) PLANE_ANGLE_UNIT ( ) SI_UNIT ( $, .RADIAN. ) );
#289=VECTOR ( 'NONE', #12464, 39.37007874015748854 ) ;
#294=DIRECTION ( 'NONE',  ( 0.000000000000000000, 0.000000000000000000, 1.000000000000000000 ) ) ;
#299=DIRECTION ( 'NONE',  ( -1.000000000000000000, -0.000000000000000000, 0.000000000000000000 ) ) ;
#304=CLOSED_SHELL ( 'NONE', ( #4084, #3715, #13988, #9132, #6250, #7556, #10908, #15018, #4095, #10366, #6449, #8320, #10443, #8270, #3227, #14480, #7146, #10275, #8252, #180, #13730, #1548, #4494, #4329, #612, #13021, #6644, #5400, #14500, #1485, #9870, #4669, #3904, #13, #9470, #71, #4566, #10359, #7820, #13323, #1048, #3821, #137, #7710, #15088, #14323, #12052, #4366, #10484, #5633, #10963, #9242, #8977, #13823, #11177, #7331, #10823, #2508, #13713, #11143, #800, #2244, #6928, #3658, #8862, #8822, #2431, #3980, #11791, #7372, #3340, #12971, #6898, #2775, #778, #5612, #40, #13581, #10360, #10036, #563, #14744, #6065, #10269, #13177, #5255, #5880, #11038, #7201, #6281, #3783, #8051, #13140, #7484, #13786, #10726, #4147, #125, #2428, #3088, #11874, #9994, #9436 ) ) ;
#305=LINE ( 'NONE', #5012, #4613 ) ;
#330=CIRCLE ( 'NONE', #3785, 2.500000000000000444 ) ;
#338=ORIENTED_EDGE ( 'NONE', *, *, #2110, .F. ) ;
#342=DIRECTION ( 'NONE',  ( -0.7071067811865406894, 0.000000000000000000, 0.7071067811865542341 ) ) ;
#346=VECTOR ( 'NONE', #13242, 39.37007874015748143 ) ;
#369=DIRECTION ( 'NONE',  ( 0.000000000000000000, 0.000000000000000000, -1.000000000000000000 ) ) ;
#370=CARTESIAN_POINT ( 'NONE',  ( 0.000000000000000000, 0.000000000000000000, 1.000000000000000000 ) ) ;
#371=AXIS2_PLACEMENT_3D ( 'NONE', #3600, #13748, #12921 ) ;
#372=LINE ( 'NONE', #5149, #13869 ) ;
#375=DIRECTION ( 'NONE',  ( -1.000000000000000000, -0.000000000000000000, 0.000000000000000000 ) ) ;
#379=ORIENTED_EDGE ( 'NONE', *, *, #8504, .T. ) ;
#380=CARTESIAN_POINT ( 'NONE',  ( 2.124999999999999556, 0.000000000000000000, 0.000000000000000000 ) ) ;
#382=LINE ( 'NONE', #600, #11482 ) ;
#389=VECTOR ( 'NONE', #6867, 39.37007874015748854 ) ;
#390=ORIENTED_EDGE ( 'NONE', *, *, #14172, .T. ) ;
#394=DIRECTION ( 'NONE',  ( 0.000000000000000000, 0.000000000000000000, -1.000000000000000000 ) ) ;
#401=AXIS2_PLACEMENT_3D ( 'NONE', #14432, #9845, #14497 ) ;
#406=DIRECTION ( 'NONE',  ( -0.000000000000000000, 1.000000000000000000, 1.224646799147353207E-16 ) ) ;
#407=DIRECTION ( 'NONE',  ( 0.000000000000000000, 0.000000000000000000, -1.000000000000000000 ) ) ;
#410=CARTESIAN_POINT ( 'NONE',  ( 2.156999999999999584, 1.679378605318042395, -1.941878605318058115 ) ) ;
#414=EDGE_CURVE ( 'NONE', #6236, #10807, #12035, .T. ) ;
#425=CARTESIAN_POINT ( 'NONE',  ( 2.774999999999999911, -1.679378605318041950, 1.679378605318059048 ) ) ;
#427=CARTESIAN_POINT ( 'NONE',  ( 2.124999999999999556, 0.9800000000000039790, 3.360000000000000320 ) ) ;
#429=ORIENTED_EDGE ( 'NONE', *, *, #6348, .F. ) ;
#432=VECTOR ( 'NONE', #14989, 39.37007874015748143 ) ;
#440=CIRCLE ( 'NONE', #11957, 0.7849999999999996980 ) ;
#448=FACE_OUTER_BOUND ( 'NONE', #12958, .T. ) ;
#451=VECTOR ( 'NONE', #6623, 39.37007874015748143 ) ;
#460=DIRECTION ( 'NONE',  ( 0.000000000000000000, 0.000000000000000000, -1.000000000000000000 ) ) ;
#461=CARTESIAN_POINT ( 'NONE',  ( 2.156999999999999140, -1.679378605318041950, 1.941878605318059003 ) ) ;
#468=EDGE_CURVE ( 'NONE', #14590, #193, #2006, .T. ) ;
#473=CARTESIAN_POINT ( 'NONE',  ( 2.650000000000001688, 1.224646799147353207E-16, 1.000000000000000000 ) ) ;
#488=CYLINDRICAL_SURFACE ( 'NONE', #3122, 1.350000000000000089 ) ;
#489=CARTESIAN_POINT ( 'NONE',  ( 2.774999999999999911, -1.679378605318041950, 1.941878605318059003 ) ) ;
#497=DIRECTION ( 'NONE',  ( -1.000000000000000000, -0.000000000000000000, -0.000000000000000000 ) ) ;
#506=CARTESIAN_POINT ( 'NONE',  ( 0.06299999999999998657, 0.000000000000000000, -1.875500000000000167 ) ) ;
#508=DIRECTION ( 'NONE',  ( -1.000000000000000000, -0.000000000000000000, -0.000000000000000000 ) ) ;
#511=CARTESIAN_POINT ( 'NONE',  ( 2.124999999999999556, -1.679378605318059048, -1.384878605318057510 ) ) ;
#518=CARTESIAN_POINT ( 'NONE',  ( 2.774999999999999911, 2.360000000000016307, 0.9799999999999454703 ) ) ;
#524=VERTEX_POINT ( 'NONE', #1618 ) ;
#531=DIRECTION ( 'NONE',  ( 1.000000000000000000, 0.000000000000000000, 0.000000000000000000 ) ) ;
#536=ORIENTED_EDGE ( 'NONE', *, *, #13800, .F. ) ;
#539=VERTEX_POINT ( 'NONE', #3171 ) ;
#552=ORIENTED_EDGE ( 'NONE', *, *, #11125, .T. ) ;
#557=VERTEX_POINT ( 'NONE', #11417 ) ;
#563=ADVANCED_FACE ( 'NONE', ( #6763 ), #8985, .F. ) ;
#572=DIRECTION ( 'NONE',  ( 1.000000000000000000, 0.000000000000000000, 0.000000000000000000 ) ) ;
#573=ORIENTED_EDGE ( 'NONE', *, *, #1982, .T. ) ;
#577=CARTESIAN_POINT ( 'NONE',  ( 2.742999999999999883, -1.679378605318041950, 1.941878605318059003 ) ) ;
#578=ORIENTED_EDGE ( 'NONE', *, *, #9901, .F. ) ;
#580=CARTESIAN_POINT ( 'NONE',  ( 2.743000000000000771, 1.679378605318059048, 1.416878605318041773 ) ) ;
#584=AXIS2_PLACEMENT_3D ( 'NONE', #12545, #6758, #756 ) ;
#589=LINE ( 'NONE', #1684, #13235 ) ;
#593=DIRECTION ( 'NONE',  ( 0.000000000000000000, 0.000000000000000000, 1.000000000000000000 ) ) ;
#598=DIRECTION ( 'NONE',  ( 0.000000000000000000, 0.000000000000000000, -1.000000000000000000 ) ) ;
#600=CARTESIAN_POINT ( 'NONE',  ( 2.775039370078740131, 1.679378605318035733, -1.304378605318064821 ) ) ;
#605=CARTESIAN_POINT ( 'NONE',  ( 2.124999999999999556, 0.000000000000000000, -1.875000000000000000 ) ) ;
#609=AXIS2_PLACEMENT_3D ( 'NONE', #12044, #1552, #6237 ) ;
#612=ADVANCED_FACE ( 'NONE', ( #3391 ), #6846, .F. ) ;
#621=LINE ( 'NONE', #5395, #4023 ) ;
#623=CARTESIAN_POINT ( 'NONE',  ( 2.774999999999999911, 1.575000000000000178, -2.360000000000016751 ) ) ;
#636=VECTOR ( 'NONE', #2663, 39.37007874015748143 ) ;
#651=VERTEX_POINT ( 'NONE', #8070 ) ;
#667=ORIENTED_EDGE ( 'NONE', *, *, #11769, .T. ) ;
#669=AXIS2_PLACEMENT_3D ( 'NONE', #11948, #9659, #8440 ) ;
#672=DIRECTION ( 'NONE',  ( -1.000000000000000000, -0.000000000000000000, -0.000000000000000000 ) ) ;
#673=ORIENTED_EDGE ( 'NONE', *, *, #277, .F. ) ;
#679=EDGE_LOOP ( 'NONE', ( #6399, #14772, #12515, #13247 ) ) ;
#703=CARTESIAN_POINT ( 'NONE',  ( 2.774999999999999911, 1.679378605318059048, 1.416878605318041773 ) ) ;
#709=CIRCLE ( 'NONE', #222, 0.3750000000000007772 ) ;
#715=FACE_OUTER_BOUND ( 'NONE', #10174, .T. ) ;
#729=ORIENTED_EDGE ( 'NONE', *, *, #3796, .F. ) ;
#730=ORIENTED_EDGE ( 'NONE', *, *, #6624, .F. ) ;
#733=VERTEX_POINT ( 'NONE', #9363 ) ;
#737=ORIENTED_EDGE ( 'NONE', *, *, #13348, .T. ) ;
#740=AXIS2_PLACEMENT_3D ( 'NONE', #2703, #375, #9368 ) ;
#750=DIRECTION ( 'NONE',  ( 0.7071067811865467956, 8.659560562354941486E-17, 0.7071067811865482389 ) ) ;
#756=DIRECTION ( 'NONE',  ( 0.000000000000000000, 0.000000000000000000, 1.000000000000000000 ) ) ;
#762=DIRECTION ( 'NONE',  ( 0.000000000000000000, 0.000000000000000000, 1.000000000000000000 ) ) ;
#774=DIRECTION ( 'NONE',  ( 0.000000000000000000, 0.000000000000000000, -1.000000000000000000 ) ) ;
#778=ADVANCED_FACE ( 'NONE', ( #1231 ), #10577, .F. ) ;
#789=LINE ( 'NONE', #5486, #7557 ) ;
#800=ADVANCED_FACE ( 'NONE', ( #6370 ), #12022, .T. ) ;
#805=EDGE_CURVE ( 'NONE', #9005, #8364, #589, .T. ) ;
#814=CARTESIAN_POINT ( 'NONE',  ( 0.09500000000000431710, 1.679378605318059492, 1.304378605318041062 ) ) ;
#817=PRODUCT_DEFINITION_FORMATION_WITH_SPECIFIED_SOURCE ( 'ANY', '', #5185, .NOT_KNOWN. ) ;
#830=CIRCLE ( 'NONE', #584, 0.9999999999999996669 ) ;
#831=EDGE_CURVE ( 'NONE', #947, #3137, #10571, .T. ) ;
#834=DIRECTION ( 'NONE',  ( 0.000000000000000000, 0.000000000000000000, -1.000000000000000000 ) ) ;
#839=CIRCLE ( 'NONE', #10405, 0.4070000000000058016 ) ;
#840=VECTOR ( 'NONE', #1217, 39.37007874015748143 ) ;
#844=ORIENTED_EDGE ( 'NONE', *, *, #11893, .T. ) ;
#845=CYLINDRICAL_SURFACE ( 'NONE', #14549, 0.2624999999999994560 ) ;
#857=CIRCLE ( 'NONE', #5772, 0.2624999999999852451 ) ;
#859=CIRCLE ( 'NONE', #6268, 2.967999999999998639 ) ;
#863=VERTEX_POINT ( 'NONE', #1533 ) ;
#868=ORIENTED_EDGE ( 'NONE', *, *, #6140, .T. ) ;
#875=CYLINDRICAL_SURFACE ( 'NONE', #13931, 0.2624999999999852451 ) ;
#878=ORIENTED_EDGE ( 'NONE', *, *, #13318, .T. ) ;
#880=ORIENTED_EDGE ( 'NONE', *, *, #3562, .T. ) ;
#883=ORIENTED_EDGE ( 'NONE', *, *, #8087, .F. ) ;
#889=EDGE_CURVE ( 'NONE', #5675, #3668, #5000, .T. ) ;
#890=CARTESIAN_POINT ( 'NONE',  ( 2.774999999999999911, -0.9799999999999436939, 3.360000000000016751 ) ) ;
#892=VECTOR ( 'NONE', #8627, 39.37007874015748143 ) ;
#900=CARTESIAN_POINT ( 'NONE',  ( 2.156999999999999584, 1.679378605318042395, -1.679378605318058604 ) ) ;
#901=CARTESIAN_POINT ( 'NONE',  ( 2.743000000000000771, 1.679378605318059048, 1.679378605318041506 ) ) ;
#903=DIRECTION ( 'NONE',  ( 0.000000000000000000, 0.000000000000000000, -1.000000000000000000 ) ) ;
#916=EDGE_CURVE ( 'NONE', #14996, #14785, #11953, .T. ) ;
#931=VECTOR ( 'NONE', #1357, 39.37007874015748143 ) ;
#937=VERTEX_POINT ( 'NONE', #5073 ) ;
#942=ORIENTED_EDGE ( 'NONE', *, *, #7538, .T. ) ;
#944=AXIS2_PLACEMENT_3D ( 'NONE', #1331, #3727, #7024 ) ;
#947=VERTEX_POINT ( 'NONE', #9877 ) ;
#948=LINE ( 'NONE', #12355, #2616 ) ;
#953=DIRECTION ( 'NONE',  ( 0.000000000000000000, 0.000000000000000000, -1.000000000000000000 ) ) ;
#955=DIRECTION ( 'NONE',  ( 0.000000000000000000, 0.000000000000000000, -1.000000000000000000 ) ) ;
#968=DIRECTION ( 'NONE',  ( -1.000000000000000000, -0.000000000000000000, -0.000000000000000000 ) ) ;
#969=VERTEX_POINT ( 'NONE', #13683 ) ;
#971=DIRECTION ( 'NONE',  ( -1.000000000000000000, -0.000000000000000000, -0.000000000000000000 ) ) ;
#976=FACE_OUTER_BOUND ( 'NONE', #152, .T. ) ;
#983=ORIENTED_EDGE ( 'NONE', *, *, #13062, .T. ) ;
#984=EDGE_LOOP ( 'NONE', ( #552, #6719 ) ) ;
#985=EDGE_CURVE ( 'NONE', #1935, #6943, #14966, .T. ) ;
#987=ORIENTED_EDGE ( 'NONE', *, *, #10256, .T. ) ;
#988=AXIS2_PLACEMENT_3D ( 'NONE', #2346, #31, #11758 ) ;
#996=DIRECTION ( 'NONE',  ( 1.000000000000000000, 0.000000000000000000, 0.000000000000000000 ) ) ;
#999=CONICAL_SURFACE ( 'NONE', #1723, 0.2624999999999852451, 0.7853981633974423948 ) ;
#1007=EDGE_CURVE ( 'NONE', #11436, #2506, #11250, .T. ) ;
#1018=DIRECTION ( 'NONE',  ( 0.000000000000000000, 0.000000000000000000, 1.000000000000000000 ) ) ;
#1019=ORIENTED_EDGE ( 'NONE', *, *, #8402, .F. ) ;
#1022=CARTESIAN_POINT ( 'NONE',  ( 0.09500000000000431710, 1.679378605318059492, 1.679378605318041506 ) ) ;
#1026=EDGE_CURVE ( 'NONE', #11415, #1104, #8866, .T. ) ;
#1028=EDGE_CURVE ( 'NONE', #539, #5425, #10488, .T. ) ;
#1039=EDGE_LOOP ( 'NONE', ( #10566, #2298 ) ) ;
#1047=AXIS2_PLACEMENT_3D ( 'NONE', #11257, #6751, #598 ) ;
#1048=ADVANCED_FACE ( 'NONE', ( #12992, #4746 ), #10329, .F. ) ;
#1052=CARTESIAN_POINT ( 'NONE',  ( 2.774999999999999911, 0.000000000000000000, 0.000000000000000000 ) ) ;
#1053=DIRECTION ( 'NONE',  ( 0.7071067811865471286, 0.000000000000000000, -0.7071067811865479058 ) ) ;
#1055=AXIS2_PLACEMENT_3D ( 'NONE', #7952, #12603, #6816 ) ;
#1058=AXIS2_PLACEMENT_3D ( 'NONE', #7084, #1237, #9450 ) ;
#1062=VERTEX_POINT ( 'NONE', #127 ) ;
#1068=AXIS2_PLACEMENT_3D ( 'NONE', #4518, #1981, #6901 ) ;
#1070=CARTESIAN_POINT ( 'NONE',  ( 2.774999999999999911, -3.360000000000016751, -0.9799999999999434719 ) ) ;
#1079=DIRECTION ( 'NONE',  ( -1.000000000000000000, -0.000000000000000000, -0.000000000000000000 ) ) ;
#1083=EDGE_CURVE ( 'NONE', #8323, #8852, #8201, .T. ) ;
#1085=CARTESIAN_POINT ( 'NONE',  ( 0.09500000000000431710, 1.679378605318059492, 1.304378605318041062 ) ) ;
#1086=CIRCLE ( 'NONE', #5244, 0.2624999999999852451 ) ;
#1091=FACE_OUTER_BOUND ( 'NONE', #12888, .T. ) ;
#1104=VERTEX_POINT ( 'NONE', #11717 ) ;
#1110=EDGE_CURVE ( 'NONE', #9095, #13586, #9853, .T. ) ;
#1114=EDGE_LOOP ( 'NONE', ( #14102, #6669, #12830, #8989 ) ) ;
#1117=EDGE_CURVE ( 'NONE', #2506, #3160, #2903, .T. ) ;
#1119=CARTESIAN_POINT ( 'NONE',  ( 0.09500000000000431710, -1.679378605318047946, -2.054378605318054163 ) ) ;
#1126=CARTESIAN_POINT ( 'NONE',  ( 0.1250000000000009992, 0.000000000000000000, 1.000000000000000000 ) ) ;
#1127=FACE_OUTER_BOUND ( 'NONE', #1598, .T. ) ;
#1130=CARTESIAN_POINT ( 'NONE',  ( 0.6179999999999965521, 1.679378605318059492, 1.304378605318041062 ) ) ;
#1132=DIRECTION ( 'NONE',  ( 1.000000000000000000, 0.000000000000000000, 0.000000000000000000 ) ) ;
#1133=DIRECTION ( 'NONE',  ( 0.000000000000000000, 0.000000000000000000, 1.000000000000000000 ) ) ;
#1138=FACE_OUTER_BOUND ( 'NONE', #7580, .T. ) ;
#1139=VECTOR ( 'NONE', #5504, 39.37007874015748143 ) ;
#1146=CARTESIAN_POINT ( 'NONE',  ( 0.06299999999999994493, 1.679378605318059492, 1.679378605318041506 ) ) ;
#1149=DIRECTION ( 'NONE',  ( 0.000000000000000000, 0.000000000000000000, -1.000000000000000000 ) ) ;
#1158=ORIENTED_EDGE ( 'NONE', *, *, #5781, .F. ) ;
#1160=VERTEX_POINT ( 'NONE', #2603 ) ;
#1171=CIRCLE ( 'NONE', #2901, 2.500000000000000000 ) ;
#1174=EDGE_LOOP ( 'NONE', ( #232, #14316, #12026, #5429 ) ) ;
#1175=AXIS2_PLACEMENT_3D ( 'NONE', #6897, #1132, #5822 ) ;
#1190=AXIS2_PLACEMENT_3D ( 'NONE', #5397, #4093, #14338 ) ;
#1193=VERTEX_POINT ( 'NONE', #10736 ) ;
#1198=VERTEX_POINT ( 'NONE', #12020 ) ;
#1206=EDGE_CURVE ( 'NONE', #10975, #1691, #225, .T. ) ;
#1217=DIRECTION ( 'NONE',  ( -1.000000000000000000, -0.000000000000000000, -0.000000000000000000 ) ) ;
#1219=ORIENTED_EDGE ( 'NONE', *, *, #5682, .F. ) ;
#1223=VERTEX_POINT ( 'NONE', #13084 ) ;
#1227=DIRECTION ( 'NONE',  ( 1.000000000000000000, 0.000000000000000000, 0.000000000000000000 ) ) ;
#1228=CARTESIAN_POINT ( 'NONE',  ( 0.06299999999999994493, 1.679378605318059492, 2.086378605318047086 ) ) ;
#1231=FACE_OUTER_BOUND ( 'NONE', #14908, .T. ) ;
#1232=CARTESIAN_POINT ( 'NONE',  ( 2.124999999999999556, -1.679378605318059048, -1.679378605318041950 ) ) ;
#1237=DIRECTION ( 'NONE',  ( -1.000000000000000000, -0.000000000000000000, -0.000000000000000000 ) ) ;
#1243=EDGE_CURVE ( 'NONE', #8971, #5394, #3645, .T. ) ;
#1250=CIRCLE ( 'NONE', #8375, 1.350000000000000089 ) ;
#1251=DIRECTION ( 'NONE',  ( 0.000000000000000000, -1.000000000000000000, 0.000000000000000000 ) ) ;
#1266=ORIENTED_EDGE ( 'NONE', *, *, #8453, .F. ) ;
#1276=LINE ( 'NONE', #4820, #14380 ) ;
#1278=CARTESIAN_POINT ( 'NONE',  ( 0.09500000000000431710, 1.679378605318035733, -1.304378605318064821 ) ) ;
#1279=EDGE_CURVE ( 'NONE', #14026, #1062, #10731, .T. ) ;
#1282=DIRECTION ( 'NONE',  ( 1.000000000000000000, 0.000000000000000000, 0.000000000000000000 ) ) ;
#1284=CARTESIAN_POINT ( 'NONE',  ( 2.124999999999999556, -1.679378605318041950, 1.679378605318059048 ) ) ;
#1297=CYLINDRICAL_SURFACE ( 'NONE', #12565, 0.3750000000000004996 ) ;
#1300=EDGE_CURVE ( 'NONE', #2080, #5889, #11936, .T. ) ;
#1305=DIRECTION ( 'NONE',  ( 0.000000000000000000, 0.000000000000000000, 1.000000000000000000 ) ) ;
#1306=DIRECTION ( 'NONE',  ( 0.000000000000000000, 0.000000000000000000, -1.000000000000000000 ) ) ;
#1308=CARTESIAN_POINT ( 'NONE',  ( 2.650000000000001688, 0.000000000000000000, 1.000000000000000000 ) ) ;
#1310=ORIENTED_EDGE ( 'NONE', *, *, #14979, .F. ) ;
#1312=DIRECTION ( 'NONE',  ( -0.000000000000000000, 4.591341165821852610E-16, -1.000000000000000000 ) ) ;
#1314=AXIS2_PLACEMENT_3D ( 'NONE', #2218, #10263, #903 ) ;
#1318=FACE_OUTER_BOUND ( 'NONE', #8544, .T. ) ;
#1319=CIRCLE ( 'NONE', #9883, 1.812500000000000222 ) ;
#1328=TOROIDAL_SURFACE ( 'NONE', #9665, 1.552690549202460968, 0.05999999999999999778 ) ;
#1330=ORIENTED_EDGE ( 'NONE', *, *, #11282, .T. ) ;
#1331=CARTESIAN_POINT ( 'NONE',  ( 0.1250000000000009992, 0.000000000000000000, 0.000000000000000000 ) ) ;
#1337=ORIENTED_EDGE ( 'NONE', *, *, #7310, .F. ) ;
#1340=ORIENTED_EDGE ( 'NONE', *, *, #12955, .T. ) ;
#1343=CARTESIAN_POINT ( 'NONE',  ( 2.774999999999999911, -1.575000000000000178, 2.360000000000016751 ) ) ;
#1357=DIRECTION ( 'NONE',  ( -1.000000000000000000, -0.000000000000000000, -0.000000000000000000 ) ) ;
#1360=EDGE_CURVE ( 'NONE', #9406, #3272, #9661, .T. ) ;
#1369=DIRECTION ( 'NONE',  ( 0.000000000000000000, 0.000000000000000000, 1.000000000000000000 ) ) ;
#1372=EDGE_CURVE ( 'NONE', #9682, #12434, #9016, .T. ) ;
#1374=VECTOR ( 'NONE', #1731, 39.37007874015748143 ) ;
#1382=LINE ( 'NONE', #11804, #13153 ) ;
#1383=ORIENTED_EDGE ( 'NONE', *, *, #3442, .T. ) ;
#1385=DIRECTION ( 'NONE',  ( -1.000000000000000000, -0.000000000000000000, -0.000000000000000000 ) ) ;
#1389=ORIENTED_EDGE ( 'NONE', *, *, #8998, .T. ) ;
#1394=DIRECTION ( 'NONE',  ( 1.000000000000000000, 0.000000000000000000, 0.000000000000000000 ) ) ;
#1395=DIRECTION ( 'NONE',  ( 1.000000000000000000, 0.000000000000000000, 0.000000000000000000 ) ) ;
#1398=CIRCLE ( 'NONE', #15093, 0.3750000000000004996 ) ;
#1404=CARTESIAN_POINT ( 'NONE',  ( 0.7100000000000001865, 0.000000000000000000, 1.552690549202460968 ) ) ;
#1417=AXIS2_PLACEMENT_3D ( 'NONE', #2473, #14168, #3540 ) ;
#1425=CARTESIAN_POINT ( 'NONE',  ( 2.775039370078740131, 1.679378605318059492, 1.679378605318041506 ) ) ;
#1428=ORIENTED_EDGE ( 'NONE', *, *, #10238, .F. ) ;
#1434=AXIS2_PLACEMENT_3D ( 'NONE', #2990, #7655, #3849 ) ;
#1445=EDGE_LOOP ( 'NONE', ( #6924, #6300, #212, #4258 ) ) ;
#1459=DIRECTION ( 'NONE',  ( -1.000000000000000000, -0.000000000000000000, -0.000000000000000000 ) ) ;
#1462=ORIENTED_EDGE ( 'NONE', *, *, #7095, .F. ) ;
#1475=LINE ( 'NONE', #6229, #346 ) ;
#1479=EDGE_LOOP ( 'NONE', ( #11498, #12621 ) ) ;
#1483=CARTESIAN_POINT ( 'NONE',  ( 0.09500000000000168032, 0.000000000000000000, 3.000000000000000444 ) ) ;
#1485=ADVANCED_FACE ( 'NONE', ( #10037 ), #2051, .F. ) ;
#1493=EDGE_LOOP ( 'NONE', ( #8132, #10838, #10009, #10420 ) ) ;
#1494=CARTESIAN_POINT ( 'NONE',  ( 2.742999999999998995, -1.679378605318059048, -1.679378605318041950 ) ) ;
#1499=EDGE_CURVE ( 'NONE', #10819, #14903, #4361, .T. ) ;
#1509=DIRECTION ( 'NONE',  ( 0.000000000000000000, 0.000000000000000000, 1.000000000000000000 ) ) ;
#1512=AXIS2_PLACEMENT_3D ( 'NONE', #901, #5372, #8962 ) ;
#1514=ORIENTED_EDGE ( 'NONE', *, *, #13348, .F. ) ;
#1521=DIRECTION ( 'NONE',  ( 1.000000000000000000, 0.000000000000000000, 0.000000000000000000 ) ) ;
#1524=AXIS2_PLACEMENT_3D ( 'NONE', #8099, #2266, #10536 ) ;
#1530=ORIENTED_EDGE ( 'NONE', *, *, #12684, .T. ) ;
#1533=CARTESIAN_POINT ( 'NONE',  ( 2.061999999999999833, 0.000000000000000000, -1.812000000000000277 ) ) ;
#1535=DIRECTION ( 'NONE',  ( -1.000000000000000000, -0.000000000000000000, -0.000000000000000000 ) ) ;
#1540=AXIS2_PLACEMENT_3D ( 'NONE', #4462, #11418, #12785 ) ;
#1547=ORIENTED_EDGE ( 'NONE', *, *, #8313, .F. ) ;
#1548=ADVANCED_FACE ( 'NONE', ( #2215 ), #3879, .F. ) ;
#1551=EDGE_CURVE ( 'NONE', #8873, #13688, #3386, .T. ) ;
#1552=DIRECTION ( 'NONE',  ( -1.000000000000000000, -0.000000000000000000, -0.000000000000000000 ) ) ;
#1554=CARTESIAN_POINT ( 'NONE',  ( 2.774999999999999911, -1.575000000000016387, -2.359999999999999876 ) ) ;
#1556=FACE_OUTER_BOUND ( 'NONE', #14489, .T. ) ;
#1557=EDGE_CURVE ( 'NONE', #5573, #10807, #10487, .T. ) ;
#1566=CONICAL_SURFACE ( 'NONE', #2319, 1.000000000000000000, 0.7853981633974488341 ) ;
#1573=DIRECTION ( 'NONE',  ( 0.000000000000000000, 0.000000000000000000, 1.000000000000000000 ) ) ;
#1581=CARTESIAN_POINT ( 'NONE',  ( 2.774999999999999911, 1.679378605318042395, -1.384878605318059952 ) ) ;
#1590=ORIENTED_EDGE ( 'NONE', *, *, #12794, .F. ) ;
#1594=DIRECTION ( 'NONE',  ( -0.7071067811865436870, 0.000000000000000000, 0.7071067811865512365 ) ) ;
#1595=AXIS2_PLACEMENT_3D ( 'NONE', #14987, #6822, #12758 ) ;
#1596=DIRECTION ( 'NONE',  ( -1.000000000000000000, -0.000000000000000000, -0.000000000000000000 ) ) ;
#1598=EDGE_LOOP ( 'NONE', ( #987, #1622, #1219, #6590 ) ) ;
#1601=CARTESIAN_POINT ( 'NONE',  ( 0.1250000000000009992, 1.224646799147353207E-16, -1.000000000000000000 ) ) ;
#1604=PLANE ( 'NONE',  #5846 ) ;
#1610=CARTESIAN_POINT ( 'NONE',  ( 0.06299999999999994493, -1.679378605318048390, 1.679378605318054163 ) ) ;
#1618=CARTESIAN_POINT ( 'NONE',  ( 0.06299999999999998657, 0.000000000000000000, -1.875500000000000167 ) ) ;
#1620=ORIENTED_EDGE ( 'NONE', *, *, #1918, .F. ) ;
#1622=ORIENTED_EDGE ( 'NONE', *, *, #5988, .F. ) ;
#1623=CARTESIAN_POINT ( 'NONE',  ( 2.124999999999999556, -1.679378605318041950, 1.679378605318059048 ) ) ;
#1625=CIRCLE ( 'NONE', #10929, 2.500000000000000444 ) ;
#1631=EDGE_CURVE ( 'NONE', #1935, #9095, #11631, .T. ) ;
#1639=EDGE_CURVE ( 'NONE', #14903, #5034, #6305, .T. ) ;
#1647=DIRECTION ( 'NONE',  ( 0.000000000000000000, 0.000000000000000000, 1.000000000000000000 ) ) ;
#1648=CARTESIAN_POINT ( 'NONE',  ( 2.774999999999999911, 0.000000000000000000, 0.000000000000000000 ) ) ;
#1652=VECTOR ( 'NONE', #3367, 39.37007874015748854 ) ;
#1657=DIRECTION ( 'NONE',  ( -0.7071067811865447972, 0.000000000000000000, 0.7071067811865501263 ) ) ;
#1659=ORIENTED_EDGE ( 'NONE', *, *, #9256, .T. ) ;
#1662=DIRECTION ( 'NONE',  ( -1.000000000000000000, -0.000000000000000000, -0.000000000000000000 ) ) ;
#1684=CARTESIAN_POINT ( 'NONE',  ( 2.775039370078740131, 1.679378605318035733, -2.054378605318066153 ) ) ;
#1691=VERTEX_POINT ( 'NONE', #6159 ) ;
#1693=EDGE_CURVE ( 'NONE', #2057, #4509, #3636, .T. ) ;
#1694=EDGE_CURVE ( 'NONE', #5675, #13385, #10717, .T. ) ;
#1698=CARTESIAN_POINT ( 'NONE',  ( 0.06299999999999994493, 1.679378605318059492, 1.679378605318041506 ) ) ;
#1701=ORIENTED_EDGE ( 'NONE', *, *, #8504, .F. ) ;
#1702=ORIENTED_EDGE ( 'NONE', *, *, #6076, .T. ) ;
#1705=ORIENTED_EDGE ( 'NONE', *, *, #1693, .T. ) ;
#1706=DIRECTION ( 'NONE',  ( 0.000000000000000000, 0.000000000000000000, -1.000000000000000000 ) ) ;
#1719=VERTEX_POINT ( 'NONE', #8603 ) ;
#1723=AXIS2_PLACEMENT_3D ( 'NONE', #3877, #8553, #2729 ) ;
#1730=CARTESIAN_POINT ( 'NONE',  ( 0.6500000000000001332, -1.679378605318048390, 1.679378605318054163 ) ) ;
#1731=DIRECTION ( 'NONE',  ( -1.000000000000000000, -0.000000000000000000, -0.000000000000000000 ) ) ;
#1734=EDGE_CURVE ( 'NONE', #937, #524, #2654, .T. ) ;
#1738=EDGE_CURVE ( 'NONE', #8382, #5425, #7069, .T. ) ;
#1741=FACE_OUTER_BOUND ( 'NONE', #2182, .T. ) ;
#1744=LINE ( 'NONE', #11085, #6232 ) ;
#1750=CYLINDRICAL_SURFACE ( 'NONE', #3389, 0.3750000000000004996 ) ;
#1754=DIRECTION ( 'NONE',  ( 0.000000000000000000, 0.000000000000000000, 1.000000000000000000 ) ) ;
#1759=AXIS2_PLACEMENT_3D ( 'NONE', #12410, #5537, #6612 ) ;
#1772=VERTEX_POINT ( 'NONE', #461 ) ;
#1774=ORIENTED_EDGE ( 'NONE', *, *, #6348, .T. ) ;
#1775=DIRECTION ( 'NONE',  ( 0.000000000000000000, 0.000000000000000000, -1.000000000000000000 ) ) ;
#1778=PLANE ( 'NONE',  #7685 ) ;
#1785=EDGE_CURVE ( 'NONE', #8971, #5110, #305, .T. ) ;
#1791=DIRECTION ( 'NONE',  ( -0.000000000000000000, 1.000000000000000000, 0.000000000000000000 ) ) ;
#1793=VERTEX_POINT ( 'NONE', #9818 ) ;
#1794=CIRCLE ( 'NONE', #6695, 0.2624999999999852451 ) ;
#1797=DIRECTION ( 'NONE',  ( -0.7071067811865422437, 0.000000000000000000, 0.7071067811865527908 ) ) ;
#1800=VECTOR ( 'NONE', #13513, 39.37007874015748854 ) ;
#1801=EDGE_CURVE ( 'NONE', #7612, #14785, #12181, .T. ) ;
#1808=VERTEX_POINT ( 'NONE', #12473 ) ;
#1818=AXIS2_PLACEMENT_3D ( 'NONE', #6677, #7746, #13765 ) ;
#1832=ORIENTED_EDGE ( 'NONE', *, *, #13509, .T. ) ;
#1835=EDGE_CURVE ( 'NONE', #3706, #11962, #3308, .T. ) ;
#1836=CARTESIAN_POINT ( 'NONE',  ( 0.6179999999999965521, 1.679378605318035733, -1.679378605318065487 ) ) ;
#1845=CIRCLE ( 'NONE', #9687, 1.000000000000000222 ) ;
#1856=EDGE_CURVE ( 'NONE', #11895, #11673, #10715, .T. ) ;
#1857=CARTESIAN_POINT ( 'NONE',  ( 2.774999999999999911, 2.399999999999999911, -0.7000000000000009548 ) ) ;
#1860=DIRECTION ( 'NONE',  ( 0.000000000000000000, 0.000000000000000000, -1.000000000000000000 ) ) ;
#1861=CIRCLE ( 'NONE', #4570, 0.2624999999999994560 ) ;
#1869=DIRECTION ( 'NONE',  ( 1.000000000000000000, 0.000000000000000000, 0.000000000000000000 ) ) ;
#1876=EDGE_CURVE ( 'NONE', #4934, #13039, #9514, .T. ) ;
#1878=CARTESIAN_POINT ( 'NONE',  ( 0.6179999999999962190, -1.679378605318048390, 2.054378605318054607 ) ) ;
#1880=CIRCLE ( 'NONE', #4091, 0.7849999999999998090 ) ;
#1885=ORIENTED_EDGE ( 'NONE', *, *, #5208, .T. ) ;
#1886=CIRCLE ( 'NONE', #12890, 0.4070000000000058016 ) ;
#1887=EDGE_LOOP ( 'NONE', ( #3497, #11766, #4798, #3666 ) ) ;
#1888=DIRECTION ( 'NONE',  ( 0.000000000000000000, 0.000000000000000000, -1.000000000000000000 ) ) ;
#1889=ORIENTED_EDGE ( 'NONE', *, *, #8087, .T. ) ;
#1895=LINE ( 'NONE', #511, #3804 ) ;
#1897=AXIS2_PLACEMENT_3D ( 'NONE', #2646, #7325, #8613 ) ;
#1898=AXIS2_PLACEMENT_3D ( 'NONE', #9262, #971, #7875 ) ;
#1903=VECTOR ( 'NONE', #3768, 39.37007874015748143 ) ;
#1907=VERTEX_POINT ( 'NONE', #9054 ) ;
#1909=CARTESIAN_POINT ( 'NONE',  ( 0.09500000000000431710, -1.679378605318047946, -1.679378605318053497 ) ) ;
#1918=EDGE_CURVE ( 'NONE', #6363, #10392, #1171, .T. ) ;
#1926=AXIS2_PLACEMENT_3D ( 'NONE', #3018, #9907, #14483 ) ;
#1930=CARTESIAN_POINT ( 'NONE',  ( 2.775039370078740131, 1.679378605318059492, 1.679378605318041506 ) ) ;
#1935=VERTEX_POINT ( 'NONE', #2069 ) ;
#1943=DIRECTION ( 'NONE',  ( -1.000000000000000000, -0.000000000000000000, -0.000000000000000000 ) ) ;
#1950=EDGE_CURVE ( 'NONE', #13688, #8873, #4111, .T. ) ;
#1964=ORIENTED_EDGE ( 'NONE', *, *, #13004, .T. ) ;
#1970=DIRECTION ( 'NONE',  ( -1.000000000000000000, -0.000000000000000000, -0.000000000000000000 ) ) ;
#1971=CARTESIAN_POINT ( 'NONE',  ( 0.1250000000000009992, 1.224646799147353207E-16, -1.000000000000000000 ) ) ;
#1972=VERTEX_POINT ( 'NONE', #10652 ) ;
#1973=DIRECTION ( 'NONE',  ( 0.000000000000000000, 0.000000000000000000, -1.000000000000000000 ) ) ;
#1975=AXIS2_PLACEMENT_3D ( 'NONE', #6108, #9693, #14267 ) ;
#1978=EDGE_LOOP ( 'NONE', ( #12904, #37, #2076, #7563 ) ) ;
#1981=DIRECTION ( 'NONE',  ( -1.000000000000000000, 0.000000000000000000, 0.000000000000000000 ) ) ;
#1982=EDGE_CURVE ( 'NONE', #5653, #11004, #3149, .T. ) ;
#1992=VERTEX_POINT ( 'NONE', #6989 ) ;
#1995=LINE ( 'NONE', #5621, #7963 ) ;
#2003=CARTESIAN_POINT ( 'NONE',  ( 2.774999999999999911, -1.679378605318059048, -1.973878605318027724 ) ) ;
#2006=CIRCLE ( 'NONE', #8148, 0.2944999999999987073 ) ;
#2007=DIRECTION ( 'NONE',  ( 0.000000000000000000, 0.000000000000000000, -1.000000000000000000 ) ) ;
#2013=CONICAL_SURFACE ( 'NONE', #1540, 0.2625000000000000111, 0.7853981633974452814 ) ;
#2033=EDGE_LOOP ( 'NONE', ( #14997, #9064, #3093, #729 ) ) ;
#2040=EDGE_LOOP ( 'NONE', ( #10640, #4681, #5070, #5535 ) ) ;
#2042=DIRECTION ( 'NONE',  ( -1.000000000000000000, -0.000000000000000000, -0.000000000000000000 ) ) ;
#2051=CYLINDRICAL_SURFACE ( 'NONE', #9263, 0.2624999999999997335 ) ;
#2056=ORIENTED_EDGE ( 'NONE', *, *, #1007, .T. ) ;
#2057=VERTEX_POINT ( 'NONE', #1228 ) ;
#2061=CIRCLE ( 'NONE', #13783, 1.000000000000000222 ) ;
#2069=CARTESIAN_POINT ( 'NONE',  ( 2.743000000000000771, 1.679378605318059048, 1.941878605318041240 ) ) ;
#2076=ORIENTED_EDGE ( 'NONE', *, *, #9463, .F. ) ;
#2077=CARTESIAN_POINT ( 'NONE',  ( 0.6500000000000001332, -1.679378605318047946, -1.679378605318053497 ) ) ;
#2079=DIRECTION ( 'NONE',  ( 0.000000000000000000, 0.000000000000000000, 1.000000000000000000 ) ) ;
#2080=VERTEX_POINT ( 'NONE', #6841 ) ;
#2084=CARTESIAN_POINT ( 'NONE',  ( 0.6179999999999965521, 1.679378605318035733, -1.679378605318065487 ) ) ;
#2086=AXIS2_PLACEMENT_3D ( 'NONE', #1730, #6700, #1018 ) ;
#2095=LINE ( 'NONE', #10370, #12837 ) ;
#2098=DIRECTION ( 'NONE',  ( 1.000000000000000000, 0.000000000000000000, 0.000000000000000000 ) ) ;
#2103=EDGE_CURVE ( 'NONE', #4450, #7612, #7070, .T. ) ;
#2104=EDGE_CURVE ( 'NONE', #4855, #12193, #5103, .T. ) ;
#2110=EDGE_CURVE ( 'NONE', #11380, #1972, #10233, .T. ) ;
#2118=ORIENTED_EDGE ( 'NONE', *, *, #14501, .T. ) ;
#2119=FACE_BOUND ( 'NONE', #5327, .T. ) ;
#2129=CARTESIAN_POINT ( 'NONE',  ( 0.6179999999999965521, 1.679378605318035733, -1.304378605318064821 ) ) ;
#2130=CYLINDRICAL_SURFACE ( 'NONE', #3086, 2.500000000000000000 ) ;
#2132=DIRECTION ( 'NONE',  ( -1.000000000000000000, -0.000000000000000000, -0.000000000000000000 ) ) ;
#2139=ORIENTED_EDGE ( 'NONE', *, *, #4405, .F. ) ;
#2141=EDGE_CURVE ( 'NONE', #8364, #1193, #9801, .T. ) ;
#2147=DIRECTION ( 'NONE',  ( -1.000000000000000000, -0.000000000000000000, -0.000000000000000000 ) ) ;
#2155=CONICAL_SURFACE ( 'NONE', #12177, 0.3750000000000007772, 0.7853981633974579379 ) ;
#2163=DIRECTION ( 'NONE',  ( 0.000000000000000000, 0.000000000000000000, -1.000000000000000000 ) ) ;
#2165=CARTESIAN_POINT ( 'NONE',  ( 2.650000000000001688, 0.000000000000000000, 0.000000000000000000 ) ) ;
#2170=DIRECTION ( 'NONE',  ( -1.000000000000000000, -0.000000000000000000, -0.000000000000000000 ) ) ;
#2178=VERTEX_POINT ( 'NONE', #13297 ) ;
#2179=CIRCLE ( 'NONE', #944, 1.000000000000000000 ) ;
#2182=EDGE_LOOP ( 'NONE', ( #1514, #7402, #9942, #283 ) ) ;
#2184=EDGE_CURVE ( 'NONE', #8852, #2297, #5354, .T. ) ;
#2197=CARTESIAN_POINT ( 'NONE',  ( 2.774999999999999911, -2.360000000000016751, -1.574999999999999956 ) ) ;
#2203=LINE ( 'NONE', #6887, #1139 ) ;
#2205=DIRECTION ( 'NONE',  ( 0.000000000000000000, 0.000000000000000000, -1.000000000000000000 ) ) ;
#2206=ORIENTED_EDGE ( 'NONE', *, *, #13800, .T. ) ;
#2211=FACE_OUTER_BOUND ( 'NONE', #7377, .T. ) ;
#2214=CARTESIAN_POINT ( 'NONE',  ( 2.774999999999999911, -0.6999999999999990674, -2.399999999999999911 ) ) ;
#2215=FACE_OUTER_BOUND ( 'NONE', #1978, .T. ) ;
#2218=CARTESIAN_POINT ( 'NONE',  ( 0.000000000000000000, 0.000000000000000000, 0.000000000000000000 ) ) ;
#2222=FACE_BOUND ( 'NONE', #13286, .T. ) ;
#2223=EDGE_LOOP ( 'NONE', ( #3449, #14253, #4944, #6407 ) ) ;
#2226=ORIENTED_EDGE ( 'NONE', *, *, #5942, .T. ) ;
#2227=AXIS2_PLACEMENT_3D ( 'NONE', #2077, #6766, #5623 ) ;
#2242=CARTESIAN_POINT ( 'NONE',  ( 2.124999999999999556, 2.360000000000016307, 0.9799999999999454703 ) ) ;
#2244=ADVANCED_FACE ( 'NONE', ( #12018 ), #8584, .F. ) ;
#2251=DIRECTION ( 'NONE',  ( 1.000000000000000000, 0.000000000000000000, 0.000000000000000000 ) ) ;
#2261=ORIENTED_EDGE ( 'NONE', *, *, #12619, .T. ) ;
#2262=CARTESIAN_POINT ( 'NONE',  ( 2.774999999999999911, 1.574999999999994849, -1.575000000000022160 ) ) ;
#2266=DIRECTION ( 'NONE',  ( 1.000000000000000000, 0.000000000000000000, 0.000000000000000000 ) ) ;
#2268=ORIENTED_EDGE ( 'NONE', *, *, #11663, .F. ) ;
#2280=DIRECTION ( 'NONE',  ( -1.000000000000000000, -0.000000000000000000, -0.000000000000000000 ) ) ;
#2289=LINE ( 'NONE', #4826, #14616 ) ;
#2293=AXIS2_PLACEMENT_3D ( 'NONE', #12771, #14073, #4758 ) ;
#2297=VERTEX_POINT ( 'NONE', #8877 ) ;
#2298=ORIENTED_EDGE ( 'NONE', *, *, #11565, .T. ) ;
#2299=CYLINDRICAL_SURFACE ( 'NONE', #2293, 3.000000000000000444 ) ;
#2315=CONICAL_SURFACE ( 'NONE', #3040, 1.000000000000000000, 0.7853981633974488341 ) ;
#2319=AXIS2_PLACEMENT_3D ( 'NONE', #14710, #10201, #3311 ) ;
#2328=AXIS2_PLACEMENT_3D ( 'NONE', #5829, #10414, #5906 ) ;
#2329=CARTESIAN_POINT ( 'NONE',  ( 0.06299999999999994493, 0.000000000000000000, 0.000000000000000000 ) ) ;
#2331=EDGE_LOOP ( 'NONE', ( #667, #4379, #10792, #5951 ) ) ;
#2332=VERTEX_POINT ( 'NONE', #11088 ) ;
#2334=AXIS2_PLACEMENT_3D ( 'NONE', #12175, #10882, #9963 ) ;
#2336=ORIENTED_EDGE ( 'NONE', *, *, #14156, .T. ) ;
#2337=DIRECTION ( 'NONE',  ( 0.000000000000000000, 0.000000000000000000, -1.000000000000000000 ) ) ;
#2346=CARTESIAN_POINT ( 'NONE',  ( 2.774999999999999911, -1.679378605318059048, -1.679378605318041950 ) ) ;
#2347=AXIS2_PLACEMENT_3D ( 'NONE', #12245, #2845, #1754 ) ;
#2352=DIRECTION ( 'NONE',  ( -1.000000000000000000, -0.000000000000000000, -0.000000000000000000 ) ) ;
#2373=DIRECTION ( 'NONE',  ( 0.000000000000000000, 0.000000000000000000, -1.000000000000000000 ) ) ;
#2382=DIRECTION ( 'NONE',  ( -1.000000000000000000, 0.000000000000000000, 0.000000000000000000 ) ) ;
#2383=FACE_OUTER_BOUND ( 'NONE', #14366, .T. ) ;
#2390=ORIENTED_EDGE ( 'NONE', *, *, #3595, .T. ) ;
#2396=VERTEX_POINT ( 'NONE', #3288 ) ;
#2401=AXIS2_PLACEMENT_3D ( 'NONE', #7870, #6806, #5431 ) ;
#2406=CARTESIAN_POINT ( 'NONE',  ( 2.124999999999999556, 1.679378605318042395, -1.384878605318058842 ) ) ;
#2416=CARTESIAN_POINT ( 'NONE',  ( 0.06299999999999994493, 3.000000000000000444, 0.000000000000000000 ) ) ;
#2422=VECTOR ( 'NONE', #14735, 39.37007874015748143 ) ;
#2425=VERTEX_POINT ( 'NONE', #53 ) ;
#2428=ADVANCED_FACE ( 'NONE', ( #11476 ), #2599, .T. ) ;
#2431=ADVANCED_FACE ( 'NONE', ( #10325 ), #2130, .T. ) ;
#2435=CARTESIAN_POINT ( 'NONE',  ( 2.774999999999999911, 1.679378605318042395, -1.679378605318058604 ) ) ;
#2441=DIRECTION ( 'NONE',  ( 0.000000000000000000, 0.000000000000000000, -1.000000000000000000 ) ) ;
#2442=ORIENTED_EDGE ( 'NONE', *, *, #11847, .F. ) ;
#2446=DIRECTION ( 'NONE',  ( 1.000000000000000000, 0.000000000000000000, 0.000000000000000000 ) ) ;
#2447=EDGE_CURVE ( 'NONE', #14903, #10819, #3568, .T. ) ;
#2449=CARTESIAN_POINT ( 'NONE',  ( 2.742999999999998995, -1.679378605318059048, -1.679378605318041950 ) ) ;
#2452=EDGE_CURVE ( 'NONE', #3716, #6251, #7725, .T. ) ;
#2457=DIRECTION ( 'NONE',  ( -1.000000000000000000, -0.000000000000000000, -0.000000000000000000 ) ) ;
#2459=ORIENTED_EDGE ( 'NONE', *, *, #5708, .T. ) ;
#2466=FACE_OUTER_BOUND ( 'NONE', #5266, .T. ) ;
#2469=EDGE_CURVE ( 'NONE', #11381, #11962, #12585, .T. ) ;
#2473=CARTESIAN_POINT ( 'NONE',  ( 0.6500000000000001332, 1.679378605318035733, -1.679378605318065487 ) ) ;
#2474=ORIENTED_EDGE ( 'NONE', *, *, #13056, .T. ) ;
#2475=CARTESIAN_POINT ( 'NONE',  ( 0.6500000000000001332, 1.679378605318035733, -1.272378605318060796 ) ) ;
#2477=CYLINDRICAL_SURFACE ( 'NONE', #5258, 1.000000000000000222 ) ;
#2493=LINE ( 'NONE', #14027, #389 ) ;
#2506=VERTEX_POINT ( 'NONE', #14915 ) ;
#2508=ADVANCED_FACE ( 'NONE', ( #12692 ), #10784, .T. ) ;
#2510=CARTESIAN_POINT ( 'NONE',  ( 0.6179999999999962190, -1.679378605318048390, 1.679378605318054163 ) ) ;
#2515=DIRECTION ( 'NONE',  ( -1.000000000000000000, -0.000000000000000000, -0.000000000000000000 ) ) ;
#2517=CARTESIAN_POINT ( 'NONE',  ( 0.000000000000000000, 0.000000000000000000, 3.000000000000000444 ) ) ;
#2529=DIRECTION ( 'NONE',  ( -1.000000000000000000, -0.000000000000000000, 0.000000000000000000 ) ) ;
#2531=VERTEX_POINT ( 'NONE', #14436 ) ;
#2549=DIRECTION ( 'NONE',  ( 0.000000000000000000, 0.000000000000000000, 1.000000000000000000 ) ) ;
#2550=ORIENTED_EDGE ( 'NONE', *, *, #11021, .T. ) ;
#2558=DIRECTION ( 'NONE',  ( 0.000000000000000000, 0.000000000000000000, -1.000000000000000000 ) ) ;
#2561=AXIS2_PLACEMENT_3D ( 'NONE', #8508, #216, #1369 ) ;
#2567=CARTESIAN_POINT ( 'NONE',  ( 0.6179999999999962190, -1.679378605318048390, 1.304378605318053497 ) ) ;
#2574=CONICAL_SURFACE ( 'NONE', #1818, 1.875000000000000000, 0.7853981633974482790 ) ;
#2580=ORIENTED_EDGE ( 'NONE', *, *, #11422, .T. ) ;
#2581=CIRCLE ( 'NONE', #11123, 0.3750000000000004996 ) ;
#2582=DIRECTION ( 'NONE',  ( -1.000000000000000000, -0.000000000000000000, -0.000000000000000000 ) ) ;
#2594=DIRECTION ( 'NONE',  ( 1.000000000000000000, 0.000000000000000000, 0.000000000000000000 ) ) ;
#2599=CONICAL_SURFACE ( 'NONE', #7470, 2.967999999999998639, 0.7853981633974482790 ) ;
#2603=CARTESIAN_POINT ( 'NONE',  ( 0.06299999999999994493, 3.654346048655701274E-16, 2.967999999999998639 ) ) ;
#2609=ORIENTED_EDGE ( 'NONE', *, *, #10633, .F. ) ;
#2616=VECTOR ( 'NONE', #3332, 39.37007874015748143 ) ;
#2623=DIRECTION ( 'NONE',  ( 0.000000000000000000, 0.000000000000000000, 1.000000000000000000 ) ) ;
#2626=DIRECTION ( 'NONE',  ( 0.000000000000000000, 0.000000000000000000, 1.000000000000000000 ) ) ;
#2643=LINE ( 'NONE', #3870, #5524 ) ;
#2644=DIRECTION ( 'NONE',  ( 0.000000000000000000, -1.000000000000000000, 0.000000000000000000 ) ) ;
#2646=CARTESIAN_POINT ( 'NONE',  ( 0.6500000000000001332, -1.679378605318048390, 1.679378605318054163 ) ) ;
#2653=VECTOR ( 'NONE', #10801, 39.37007874015748854 ) ;
#2654=CIRCLE ( 'NONE', #11200, 1.875500000000000167 ) ;
#2655=CONICAL_SURFACE ( 'NONE', #11707, 1.875000000000000000, 0.7853981633974482790 ) ;
#2658=ORIENTED_EDGE ( 'NONE', *, *, #14455, .F. ) ;
#2663=DIRECTION ( 'NONE',  ( 0.000000000000000000, -1.000000000000000000, 0.000000000000000000 ) ) ;
#2664=ORIENTED_EDGE ( 'NONE', *, *, #8629, .F. ) ;
#2671=DIRECTION ( 'NONE',  ( 0.000000000000000000, 0.000000000000000000, 1.000000000000000000 ) ) ;
#2676=CARTESIAN_POINT ( 'NONE',  ( 2.774999999999999911, -1.574999999999984190, 1.575000000000033040 ) ) ;
#2684=EDGE_LOOP ( 'NONE', ( #2658, #13898, #14726, #8637 ) ) ;
#2698=EDGE_CURVE ( 'NONE', #1992, #11318, #4553, .T. ) ;
#2703=CARTESIAN_POINT ( 'NONE',  ( 2.774999999999999911, -3.360000000000000320, 0.9799999999999999822 ) ) ;
#2704=DIRECTION ( 'NONE',  ( 0.7071067811865474617, 0.000000000000000000, -0.7071067811865474617 ) ) ;
#2705=ORIENTED_EDGE ( 'NONE', *, *, #1557, .F. ) ;
#2719=DIRECTION ( 'NONE',  ( -0.7071067811865414665, 8.659560562355006814E-17, -0.7071067811865534569 ) ) ;
#2727=CARTESIAN_POINT ( 'NONE',  ( 2.774999999999999911, 0.9799999999999438050, -2.360000000000016307 ) ) ;
#2728=CARTESIAN_POINT ( 'NONE',  ( 2.156999999999998696, -1.679378605318059048, -1.941878605318027251 ) ) ;
#2729=DIRECTION ( 'NONE',  ( 0.000000000000000000, 0.000000000000000000, -1.000000000000000000 ) ) ;
#2734=DIRECTION ( 'NONE',  ( -0.7071067811865376918, 0.000000000000000000, 0.7071067811865573427 ) ) ;
#2735=DIRECTION ( 'NONE',  ( 1.000000000000000000, 0.000000000000000000, 0.000000000000000000 ) ) ;
#2738=ORIENTED_EDGE ( 'NONE', *, *, #8998, .F. ) ;
#2741=EDGE_CURVE ( 'NONE', #1223, #7612, #12351, .T. ) ;
#2742=LINE ( 'NONE', #1278, #11744 ) ;
#2747=DIRECTION ( 'NONE',  ( 0.000000000000000000, 0.000000000000000000, 1.000000000000000000 ) ) ;
#2749=CARTESIAN_POINT ( 'NONE',  ( 2.124999999999999556, -0.9799999999999436939, 2.360000000000016307 ) ) ;
#2750=CARTESIAN_POINT ( 'NONE',  ( 0.6179999999999962190, -1.679378605318048390, 1.679378605318054163 ) ) ;
#2751=ORIENTED_EDGE ( 'NONE', *, *, #233, .T. ) ;
#2752=ORIENTED_EDGE ( 'NONE', *, *, #14636, .F. ) ;
#2758=AXIS2_PLACEMENT_3D ( 'NONE', #3900, #13061, #3826 ) ;
#2762=DIRECTION ( 'NONE',  ( 1.000000000000000000, 0.000000000000000000, 0.000000000000000000 ) ) ;
#2766=CARTESIAN_POINT ( 'NONE',  ( 2.774999999999999911, 0.000000000000000000, 0.000000000000000000 ) ) ;
#2767=CARTESIAN_POINT ( 'NONE',  ( 2.743000000000000327, 1.679378605318042395, -1.941878605318058115 ) ) ;
#2773=EDGE_CURVE ( 'NONE', #3609, #5110, #5774, .T. ) ;
#2775=ADVANCED_FACE ( 'NONE', ( #1091 ), #15101, .F. ) ;
#2786=CIRCLE ( 'NONE', #5229, 1.350000000000000089 ) ;
#2791=DIRECTION ( 'NONE',  ( 0.000000000000000000, -4.591341165822158293E-16, 1.000000000000000000 ) ) ;
#2797=EDGE_CURVE ( 'NONE', #13738, #4021, #14499, .T. ) ;
#2801=EDGE_CURVE ( 'NONE', #1793, #1160, #859, .T. ) ;
#2804=CARTESIAN_POINT ( 'NONE',  ( 0.000000000000000000, 0.000000000000000000, 1.125000000000000888 ) ) ;
#2828=VERTEX_POINT ( 'NONE', #17 ) ;
#2830=CONICAL_SURFACE ( 'NONE', #2334, 0.3750000000000004996, 0.7853981633974503884 ) ;
#2831=CARTESIAN_POINT ( 'NONE',  ( 2.774999999999999911, 0.000000000000000000, 0.000000000000000000 ) ) ;
#2834=DIRECTION ( 'NONE',  ( 0.000000000000000000, 9.182682331643740718E-16, -1.000000000000000000 ) ) ;
#2843=AXIS2_PLACEMENT_3D ( 'NONE', #7989, #14944, #6851 ) ;
#2845=DIRECTION ( 'NONE',  ( -1.000000000000000000, -0.000000000000000000, -0.000000000000000000 ) ) ;
#2858=ORIENTED_EDGE ( 'NONE', *, *, #1785, .F. ) ;
#2869=CARTESIAN_POINT ( 'NONE',  ( 2.124999999999999556, 0.000000000000000000, 0.000000000000000000 ) ) ;
#2870=EDGE_CURVE ( 'NONE', #11436, #11127, #242, .T. ) ;
#2873=ORIENTED_EDGE ( 'NONE', *, *, #14209, .T. ) ;
#2875=ORIENTED_EDGE ( 'NONE', *, *, #5133, .F. ) ;
#2880=EDGE_CURVE ( 'NONE', #3585, #7387, #1475, .T. ) ;
#2888=AXIS2_PLACEMENT_3D ( 'NONE', #6380, #531, #4077 ) ;
#2901=AXIS2_PLACEMENT_3D ( 'NONE', #8897, #11263, #834 ) ;
#2903=CIRCLE ( 'NONE', #11453, 0.2944999999999998175 ) ;
#2907=DIRECTION ( 'NONE',  ( 0.000000000000000000, 0.000000000000000000, 1.000000000000000000 ) ) ;
#2911=DIRECTION ( 'NONE',  ( 0.000000000000000000, 0.000000000000000000, -1.000000000000000000 ) ) ;
#2920=CONICAL_SURFACE ( 'NONE', #14389, 0.3750000000000004996, 0.7853981633974557175 ) ;
#2925=FACE_OUTER_BOUND ( 'NONE', #11558, .T. ) ;
#2928=ORIENTED_EDGE ( 'NONE', *, *, #171, .F. ) ;
#2944=DIRECTION ( 'NONE',  ( -1.000000000000000000, -0.000000000000000000, -0.000000000000000000 ) ) ;
#2953=DIRECTION ( 'NONE',  ( 0.000000000000000000, 0.000000000000000000, -1.000000000000000000 ) ) ;
#2964=EDGE_CURVE ( 'NONE', #9941, #7401, #2061, .T. ) ;
#2979=DIRECTION ( 'NONE',  ( 1.000000000000000000, 0.000000000000000000, 0.000000000000000000 ) ) ;
#2990=CARTESIAN_POINT ( 'NONE',  ( 0.6179999999999965521, -1.679378605318047946, -1.679378605318053497 ) ) ;
#2991=EDGE_CURVE ( 'NONE', #6614, #539, #12255, .T. ) ;
#2997=CARTESIAN_POINT ( 'NONE',  ( 0.09500000000000431710, -1.679378605318048390, 1.304378605318053497 ) ) ;
#3000=VECTOR ( 'NONE', #13226, 39.37007874015748143 ) ;
#3008=DIRECTION ( 'NONE',  ( 1.000000000000000000, 0.000000000000000000, 0.000000000000000000 ) ) ;
#3013=FACE_OUTER_BOUND ( 'NONE', #133, .T. ) ;
#3018=CARTESIAN_POINT ( 'NONE',  ( 2.124999999999999556, 1.575000000000016609, 1.575000000000000178 ) ) ;
#3033=CIRCLE ( 'NONE', #1314, 1.125000000000000888 ) ;
#3040=AXIS2_PLACEMENT_3D ( 'NONE', #2165, #4989, #6853 ) ;
#3055=CARTESIAN_POINT ( 'NONE',  ( 0.6179999999999965521, -1.679378605318047946, -1.304378605318053053 ) ) ;
#3060=VECTOR ( 'NONE', #14384, 39.37007874015748143 ) ;
#3079=( NAMED_UNIT ( * ) SI_UNIT ( $, .STERADIAN. ) SOLID_ANGLE_UNIT ( ) );
#3085=CARTESIAN_POINT ( 'NONE',  ( 2.774999999999999911, 0.000000000000000000, 0.000000000000000000 ) ) ;
#3086=AXIS2_PLACEMENT_3D ( 'NONE', #1052, #14060, #11549 ) ;
#3088=ADVANCED_FACE ( 'NONE', ( #8827 ), #1566, .F. ) ;
#3093=ORIENTED_EDGE ( 'NONE', *, *, #1950, .T. ) ;
#3094=ORIENTED_EDGE ( 'NONE', *, *, #8858, .F. ) ;
#3095=CARTESIAN_POINT ( 'NONE',  ( 2.774999999999999911, 1.679378605318042395, -1.973878605318057478 ) ) ;
#3096=VERTEX_POINT ( 'NONE', #14859 ) ;
#3099=CARTESIAN_POINT ( 'NONE',  ( 2.124999999999999556, -0.6999999999999990674, -2.399999999999999911 ) ) ;
#3109=ORIENTED_EDGE ( 'NONE', *, *, #8595, .T. ) ;
#3111=ORIENTED_EDGE ( 'NONE', *, *, #5141, .T. ) ;
#3114=CARTESIAN_POINT ( 'NONE',  ( 2.124999999999999556, -2.400000000000011902, -0.6999999999999596545 ) ) ;
#3118=DIRECTION ( 'NONE',  ( -1.000000000000000000, -0.000000000000000000, -0.000000000000000000 ) ) ;
#3120=DIRECTION ( 'NONE',  ( 1.000000000000000000, 0.000000000000000000, 0.000000000000000000 ) ) ;
#3122=AXIS2_PLACEMENT_3D ( 'NONE', #7409, #3894, #1573 ) ;
#3135=CYLINDRICAL_SURFACE ( 'NONE', #3369, 0.3750000000000007772 ) ;
#3136=CARTESIAN_POINT ( 'NONE',  ( 2.124999999999999556, 1.679378605318042395, -1.679378605318058604 ) ) ;
#3137=VERTEX_POINT ( 'NONE', #5460 ) ;
#3138=CYLINDRICAL_SURFACE ( 'NONE', #13116, 0.7849999999999998090 ) ;
#3143=VECTOR ( 'NONE', #11016, 39.37007874015748143 ) ;
#3149=CIRCLE ( 'NONE', #4868, 0.4070000000000046914 ) ;
#3156=ORIENTED_EDGE ( 'NONE', *, *, #1876, .T. ) ;
#3158=DIRECTION ( 'NONE',  ( 1.000000000000000000, 0.000000000000000000, 0.000000000000000000 ) ) ;
#3160=VERTEX_POINT ( 'NONE', #10127 ) ;
#3167=DIRECTION ( 'NONE',  ( 0.000000000000000000, 0.000000000000000000, -1.000000000000000000 ) ) ;
#3171=CARTESIAN_POINT ( 'NONE',  ( 1.375000000000000000, 1.653273178848927113E-16, -1.350000000000000089 ) ) ;
#3206=FACE_BOUND ( 'NONE', #5790, .T. ) ;
#3214=CARTESIAN_POINT ( 'NONE',  ( 2.156999999999999584, 1.679378605318059048, 1.416878605318041773 ) ) ;
#3216=EDGE_LOOP ( 'NONE', ( #10092, #7677, #14280, #12469 ) ) ;
#3227=ADVANCED_FACE ( 'NONE', ( #3632 ), #6994, .F. ) ;
#3239=DIRECTION ( 'NONE',  ( -1.000000000000000000, -0.000000000000000000, -0.000000000000000000 ) ) ;
#3240=ORIENTED_EDGE ( 'NONE', *, *, #198, .F. ) ;
#3242=DIRECTION ( 'NONE',  ( -1.000000000000000000, 0.000000000000000000, -0.000000000000000000 ) ) ;
#3248=ORIENTED_EDGE ( 'NONE', *, *, #46, .T. ) ;
#3252=EDGE_CURVE ( 'NONE', #9941, #1198, #4628, .T. ) ;
#3267=CIRCLE ( 'NONE', #8884, 0.3750000000000004996 ) ;
#3272=VERTEX_POINT ( 'NONE', #9453 ) ;
#3276=ORIENTED_EDGE ( 'NONE', *, *, #889, .T. ) ;
#3280=CARTESIAN_POINT ( 'NONE',  ( 2.775039370078740131, 1.679378605318035733, -1.679378605318065487 ) ) ;
#3282=CARTESIAN_POINT ( 'NONE',  ( 2.775039370078740131, -1.679378605318048390, 1.304378605318053497 ) ) ;
#3283=ORIENTED_EDGE ( 'NONE', *, *, #2801, .F. ) ;
#3284=CARTESIAN_POINT ( 'NONE',  ( 0.06299999999999994493, -1.679378605318047946, -2.086378605318059076 ) ) ;
#3286=CARTESIAN_POINT ( 'NONE',  ( 2.774999999999999911, -1.575000000000016387, -2.359999999999999876 ) ) ;
#3288=CARTESIAN_POINT ( 'NONE',  ( 2.774999999999999911, -0.9799999999999990941, -2.359999999999999876 ) ) ;
#3290=CYLINDRICAL_SURFACE ( 'NONE', #12054, 0.2625000000000000111 ) ;
#3297=EDGE_LOOP ( 'NONE', ( #4396, #4217 ) ) ;
#3298=ORIENTED_EDGE ( 'NONE', *, *, #1028, .T. ) ;
#3306=FACE_OUTER_BOUND ( 'NONE', #12101, .T. ) ;
#3308=LINE ( 'NONE', #6609, #8763 ) ;
#3311=DIRECTION ( 'NONE',  ( 0.000000000000000000, 0.000000000000000000, -1.000000000000000000 ) ) ;
#3313=VECTOR ( 'NONE', #12303, 39.37007874015748143 ) ;
#3315=ORIENTED_EDGE ( 'NONE', *, *, #14833, .T. ) ;
#3317=ORIENTED_EDGE ( 'NONE', *, *, #1801, .F. ) ;
#3321=DIRECTION ( 'NONE',  ( -1.000000000000000000, -0.000000000000000000, -0.000000000000000000 ) ) ;
#3322=DIRECTION ( 'NONE',  ( -0.7071067811865441310, 0.000000000000000000, 0.7071067811865509034 ) ) ;
#3330=DIRECTION ( 'NONE',  ( -1.000000000000000000, -0.000000000000000000, -0.000000000000000000 ) ) ;
#3332=DIRECTION ( 'NONE',  ( 0.000000000000000000, 1.000000000000000000, 4.591341165822158293E-16 ) ) ;
#3334=DIRECTION ( 'NONE',  ( 0.000000000000000000, 0.000000000000000000, -1.000000000000000000 ) ) ;
#3336=ORIENTED_EDGE ( 'NONE', *, *, #1738, .F. ) ;
#3340=ADVANCED_FACE ( 'NONE', ( #8152 ), #5771, .F. ) ;
#3346=ORIENTED_EDGE ( 'NONE', *, *, #10083, .T. ) ;
#3357=CARTESIAN_POINT ( 'NONE',  ( 0.000000000000000000, 0.000000000000000000, 0.000000000000000000 ) ) ;
#3358=EDGE_LOOP ( 'NONE', ( #1266, #9044, #13835, #11931 ) ) ;
#3367=DIRECTION ( 'NONE',  ( -0.7071067811865455743, 8.659560562354955045E-17, -0.7071067811865493491 ) ) ;
#3369=AXIS2_PLACEMENT_3D ( 'NONE', #3280, #7945, #10098 ) ;
#3370=DIRECTION ( 'NONE',  ( 0.000000000000000000, 0.000000000000000000, -1.000000000000000000 ) ) ;
#3376=EDGE_CURVE ( 'NONE', #2332, #5034, #839, .T. ) ;
#3379=DIRECTION ( 'NONE',  ( 0.000000000000000000, 0.000000000000000000, -1.000000000000000000 ) ) ;
#3386=CIRCLE ( 'NONE', #8289, 3.000000000000000444 ) ;
#3389=AXIS2_PLACEMENT_3D ( 'NONE', #6217, #14314, #11025 ) ;
#3391=FACE_OUTER_BOUND ( 'NONE', #4170, .T. ) ;
#3405=VECTOR ( 'NONE', #4883, 39.37007874015748143 ) ;
#3411=AXIS2_PLACEMENT_3D ( 'NONE', #623, #7608, #10981 ) ;
#3414=DIRECTION ( 'NONE',  ( 0.000000000000000000, 0.000000000000000000, -1.000000000000000000 ) ) ;
#3416=FACE_BOUND ( 'NONE', #1479, .T. ) ;
#3425=ORIENTED_EDGE ( 'NONE', *, *, #1499, .F. ) ;
#3430=EDGE_LOOP ( 'NONE', ( #82, #7939, #3111, #10078 ) ) ;
#3432=EDGE_CURVE ( 'NONE', #5425, #8382, #10884, .T. ) ;
#3440=CARTESIAN_POINT ( 'NONE',  ( 2.743000000000000327, 1.679378605318042395, -1.679378605318058604 ) ) ;
#3442=EDGE_CURVE ( 'NONE', #1719, #6236, #1895, .T. ) ;
#3444=CARTESIAN_POINT ( 'NONE',  ( 0.09500000000000431710, -1.679378605318048390, 1.679378605318054163 ) ) ;
#3445=DIRECTION ( 'NONE',  ( 0.000000000000000000, 0.000000000000000000, -1.000000000000000000 ) ) ;
#3449=ORIENTED_EDGE ( 'NONE', *, *, #14099, .F. ) ;
#3453=ORIENTED_EDGE ( 'NONE', *, *, #12031, .T. ) ;
#3466=DIRECTION ( 'NONE',  ( -1.000000000000000000, 0.000000000000000000, 0.000000000000000000 ) ) ;
#3468=EDGE_CURVE ( 'NONE', #12193, #947, #7645, .T. ) ;
#3471=DIRECTION ( 'NONE',  ( -1.000000000000000000, -0.000000000000000000, -0.000000000000000000 ) ) ;
#3477=CARTESIAN_POINT ( 'NONE',  ( 2.775039370078740131, -1.679378605318048390, 1.679378605318054163 ) ) ;
#3483=ORIENTED_EDGE ( 'NONE', *, *, #277, .T. ) ;
#3485=ORIENTED_EDGE ( 'NONE', *, *, #3252, .F. ) ;
#3497=ORIENTED_EDGE ( 'NONE', *, *, #14501, .F. ) ;
#3500=ORIENTED_EDGE ( 'NONE', *, *, #12684, .F. ) ;
#3502=ORIENTED_EDGE ( 'NONE', *, *, #1835, .T. ) ;
#3507=ORIENTED_EDGE ( 'NONE', *, *, #2447, .F. ) ;
#3511=CIRCLE ( 'NONE', #7423, 0.9999999999999996669 ) ;
#3517=CARTESIAN_POINT ( 'NONE',  ( 1.375000000000000000, 0.000000000000000000, 0.000000000000000000 ) ) ;
#3518=EDGE_CURVE ( 'NONE', #13670, #1691, #2581, .T. ) ;
#3520=DIRECTION ( 'NONE',  ( -0.9781476007338071321, 2.546183866652743860E-17, -0.2079116908177521816 ) ) ;
#3523=CARTESIAN_POINT ( 'NONE',  ( 2.774999999999999911, 2.359999999999994547, -1.575000000000016831 ) ) ;
#3524=DIRECTION ( 'NONE',  ( 0.000000000000000000, 0.000000000000000000, 1.000000000000000000 ) ) ;
#3527=DIRECTION ( 'NONE',  ( 0.000000000000000000, 0.000000000000000000, 1.000000000000000000 ) ) ;
#3540=DIRECTION ( 'NONE',  ( 0.000000000000000000, 0.000000000000000000, 1.000000000000000000 ) ) ;
#3549=CARTESIAN_POINT ( 'NONE',  ( 2.124999999999999556, 0.000000000000000000, 0.000000000000000000 ) ) ;
#3556=CARTESIAN_POINT ( 'NONE',  ( 0.06299999999999994493, 1.679378605318035733, -1.679378605318065487 ) ) ;
#3557=AXIS2_PLACEMENT_3D ( 'NONE', #12, #15020, #7161 ) ;
#3562=EDGE_CURVE ( 'NONE', #1972, #7174, #9678, .T. ) ;
#3568=CIRCLE ( 'NONE', #9915, 0.3750000000000004996 ) ;
#3573=ORIENTED_EDGE ( 'NONE', *, *, #13372, .T. ) ;
#3574=DIRECTION ( 'NONE',  ( 0.000000000000000000, 0.000000000000000000, -1.000000000000000000 ) ) ;
#3583=CARTESIAN_POINT ( 'NONE',  ( 2.743000000000000771, 1.679378605318059048, 1.416878605318041773 ) ) ;
#3585=VERTEX_POINT ( 'NONE', #11470 ) ;
#3587=EDGE_LOOP ( 'NONE', ( #6462, #7611, #13760, #10593 ) ) ;
#3592=ORIENTED_EDGE ( 'NONE', *, *, #2801, .T. ) ;
#3593=DIRECTION ( 'NONE',  ( 1.000000000000000000, 0.000000000000000000, 0.000000000000000000 ) ) ;
#3595=EDGE_CURVE ( 'NONE', #11724, #13670, #9101, .T. ) ;
#3600=CARTESIAN_POINT ( 'NONE',  ( 2.061999999999999389, 0.000000000000000000, 0.000000000000000000 ) ) ;
#3602=CIRCLE ( 'NONE', #10440, 0.4070000000000044138 ) ;
#3609=VERTEX_POINT ( 'NONE', #3284 ) ;
#3610=CARTESIAN_POINT ( 'NONE',  ( 0.7100000000000001865, 0.000000000000000000, 0.000000000000000000 ) ) ;
#3617=DIRECTION ( 'NONE',  ( 0.000000000000000000, 0.000000000000000000, 1.000000000000000000 ) ) ;
#3623=CARTESIAN_POINT ( 'NONE',  ( 2.743000000000000771, 1.679378605318059048, 1.679378605318041506 ) ) ;
#3627=VECTOR ( 'NONE', #5777, 39.37007874015748143 ) ;
#3632=FACE_OUTER_BOUND ( 'NONE', #12931, .T. ) ;
#3636=CIRCLE ( 'NONE', #7309, 0.4070000000000055240 ) ;
#3645=CIRCLE ( 'NONE', #12183, 0.3750000000000004996 ) ;
#3647=FACE_BOUND ( 'NONE', #15115, .T. ) ;
#3653=VECTOR ( 'NONE', #9394, 39.37007874015748143 ) ;
#3658=ADVANCED_FACE ( 'NONE', ( #9032 ), #3138, .T. ) ;
#3666=ORIENTED_EDGE ( 'NONE', *, *, #6916, .F. ) ;
#3668=VERTEX_POINT ( 'NONE', #1126 ) ;
#3670=EDGE_LOOP ( 'NONE', ( #14154, #12414, #5622, #9980 ) ) ;
#3671=DIRECTION ( 'NONE',  ( 0.000000000000000000, 0.000000000000000000, 1.000000000000000000 ) ) ;
#3674=ORIENTED_EDGE ( 'NONE', *, *, #985, .F. ) ;
#3675=LINE ( 'NONE', #2517, #892 ) ;
#3680=FACE_OUTER_BOUND ( 'NONE', #10428, .T. ) ;
#3683=EDGE_CURVE ( 'NONE', #14092, #8852, #5813, .T. ) ;
#3695=DIRECTION ( 'NONE',  ( -1.000000000000000000, 0.000000000000000000, -0.000000000000000000 ) ) ;
#3701=CARTESIAN_POINT ( 'NONE',  ( 2.124999999999999556, 1.679378605318059048, 1.679378605318041506 ) ) ;
#3706=VERTEX_POINT ( 'NONE', #6121 ) ;
#3715=ADVANCED_FACE ( 'NONE', ( #12912 ), #13347, .F. ) ;
#3716=VERTEX_POINT ( 'NONE', #14052 ) ;
#3723=EDGE_CURVE ( 'NONE', #8323, #261, #1880, .T. ) ;
#3724=CARTESIAN_POINT ( 'NONE',  ( 2.774999999999999911, 0.6999999999999599876, -2.400000000000011458 ) ) ;
#3727=DIRECTION ( 'NONE',  ( -1.000000000000000000, 0.000000000000000000, 0.000000000000000000 ) ) ;
#3745=CARTESIAN_POINT ( 'NONE',  ( 2.774999999999999911, -1.574999999999984190, 1.575000000000033040 ) ) ;
#3764=EDGE_CURVE ( 'NONE', #6889, #14179, #6780, .T. ) ;
#3766=CARTESIAN_POINT ( 'NONE',  ( 2.774999999999999911, -2.360000000000000320, 0.9799999999999999822 ) ) ;
#3768=DIRECTION ( 'NONE',  ( -1.000000000000000000, -0.000000000000000000, -0.000000000000000000 ) ) ;
#3770=DIRECTION ( 'NONE',  ( -1.000000000000000000, -0.000000000000000000, -0.000000000000000000 ) ) ;
#3774=CARTESIAN_POINT ( 'NONE',  ( 2.774999999999999911, 3.360000000000016751, 0.9799999999999461364 ) ) ;
#3782=FACE_OUTER_BOUND ( 'NONE', #11353, .T. ) ;
#3783=ADVANCED_FACE ( 'NONE', ( #15140 ), #7759, .F. ) ;
#3785=AXIS2_PLACEMENT_3D ( 'NONE', #2831, #2979, #5273 ) ;
#3792=LINE ( 'NONE', #6392, #5672 ) ;
#3796=EDGE_CURVE ( 'NONE', #6889, #8873, #3675, .T. ) ;
#3799=DIRECTION ( 'NONE',  ( -1.000000000000000000, -0.000000000000000000, -0.000000000000000000 ) ) ;
#3804=VECTOR ( 'NONE', #7233, 39.37007874015748854 ) ;
#3807=AXIS2_PLACEMENT_3D ( 'NONE', #12318, #13380, #12466 ) ;
#3819=AXIS2_PLACEMENT_3D ( 'NONE', #132, #2457, #3524 ) ;
#3821=ADVANCED_FACE ( 'NONE', ( #13494 ), #488, .T. ) ;
#3824=AXIS2_PLACEMENT_3D ( 'NONE', #7017, #11672, #1775 ) ;
#3826=DIRECTION ( 'NONE',  ( 0.000000000000000000, 0.000000000000000000, 1.000000000000000000 ) ) ;
#3830=AXIS2_PLACEMENT_3D ( 'NONE', #11236, #13814, #1888 ) ;
#3835=ORIENTED_EDGE ( 'NONE', *, *, #9491, .F. ) ;
#3841=AXIS2_PLACEMENT_3D ( 'NONE', #13951, #1251, #3414 ) ;
#3849=DIRECTION ( 'NONE',  ( 0.000000000000000000, 0.000000000000000000, -1.000000000000000000 ) ) ;
#3855=EDGE_CURVE ( 'NONE', #10392, #11506, #13605, .T. ) ;
#3870=CARTESIAN_POINT ( 'NONE',  ( 0.6180000000000012150, 0.000000000000000000, 3.000000000000000444 ) ) ;
#3877=CARTESIAN_POINT ( 'NONE',  ( 2.742999999999998995, -1.679378605318059048, -1.679378605318041950 ) ) ;
#3879=CONICAL_SURFACE ( 'NONE', #12894, 0.2944999999999998175, 0.7853981633974530530 ) ;
#3883=ORIENTED_EDGE ( 'NONE', *, *, #3376, .T. ) ;
#3886=LINE ( 'NONE', #14274, #12866 ) ;
#3894=DIRECTION ( 'NONE',  ( -1.000000000000000000, -0.000000000000000000, -0.000000000000000000 ) ) ;
#3900=CARTESIAN_POINT ( 'NONE',  ( 0.6179999999999965521, 1.679378605318035733, -1.679378605318065487 ) ) ;
#3904=ADVANCED_FACE ( 'NONE', ( #4033 ), #5044, .T. ) ;
#3906=EDGE_CURVE ( 'NONE', #2828, #9755, #8699, .T. ) ;
#3917=FACE_OUTER_BOUND ( 'NONE', #14203, .T. ) ;
#3920=CARTESIAN_POINT ( 'NONE',  ( 0.09500000000000431710, 1.679378605318035733, -2.054378605318066153 ) ) ;
#3940=ORIENTED_EDGE ( 'NONE', *, *, #13641, .T. ) ;
#3943=CYLINDRICAL_SURFACE ( 'NONE', #4578, 0.9999999999999996669 ) ;
#3953=EDGE_LOOP ( 'NONE', ( #6954, #13050, #5351, #3500 ) ) ;
#3963=CARTESIAN_POINT ( 'NONE',  ( 0.09500000000000431710, 1.679378605318059492, 2.054378605318042172 ) ) ;
#3965=DIRECTION ( 'NONE',  ( 0.000000000000000000, 0.000000000000000000, -1.000000000000000000 ) ) ;
#3968=AXIS2_PLACEMENT_3D ( 'NONE', #2766, #3986, #8444 ) ;
#3969=ORIENTED_EDGE ( 'NONE', *, *, #468, .T. ) ;
#3970=DIRECTION ( 'NONE',  ( 0.000000000000000000, 0.000000000000000000, 1.000000000000000000 ) ) ;
#3980=ADVANCED_FACE ( 'NONE', ( #5253 ), #13426, .F. ) ;
#3986=DIRECTION ( 'NONE',  ( -1.000000000000000000, -0.000000000000000000, -0.000000000000000000 ) ) ;
#3989=EDGE_CURVE ( 'NONE', #7401, #4697, #5415, .T. ) ;
#3993=ORIENTED_EDGE ( 'NONE', *, *, #5124, .F. ) ;
#4012=DIRECTION ( 'NONE',  ( 0.7071067811865436870, 0.000000000000000000, -0.7071067811865512365 ) ) ;
#4019=CARTESIAN_POINT ( 'NONE',  ( 2.774999999999999911, 1.679378605318059048, 1.384878605318042855 ) ) ;
#4021=VERTEX_POINT ( 'NONE', #9429 ) ;
#4023=VECTOR ( 'NONE', #12558, 39.37007874015748143 ) ;
#4025=CARTESIAN_POINT ( 'NONE',  ( 2.742999999999998995, -1.679378605318059048, -1.416878605318056872 ) ) ;
#4028=DIRECTION ( 'NONE',  ( 0.000000000000000000, 0.000000000000000000, 1.000000000000000000 ) ) ;
#4033=FACE_OUTER_BOUND ( 'NONE', #2033, .T. ) ;
#4035=CARTESIAN_POINT ( 'NONE',  ( 0.06299999999999994493, 0.000000000000000000, 0.000000000000000000 ) ) ;
#4053=EDGE_LOOP ( 'NONE', ( #14189, #4242, #2664, #1832 ) ) ;
#4058=DIRECTION ( 'NONE',  ( 0.000000000000000000, 0.000000000000000000, 1.000000000000000000 ) ) ;
#4077=DIRECTION ( 'NONE',  ( 0.000000000000000000, 0.000000000000000000, -1.000000000000000000 ) ) ;
#4081=LINE ( 'NONE', #8749, #7895 ) ;
#4084=ADVANCED_FACE ( 'NONE', ( #6056 ), #10948, .F. ) ;
#4088=VERTEX_POINT ( 'NONE', #11726 ) ;
#4091=AXIS2_PLACEMENT_3D ( 'NONE', #3745, #3593, #9487 ) ;
#4093=DIRECTION ( 'NONE',  ( -1.000000000000000000, 0.000000000000000000, 0.000000000000000000 ) ) ;
#4095=ADVANCED_FACE ( 'NONE', ( #214 ), #11428, .F. ) ;
#4098=CARTESIAN_POINT ( 'NONE',  ( 2.743000000000000327, 1.679378605318042395, -1.416878605318059314 ) ) ;
#4101=VERTEX_POINT ( 'NONE', #9582 ) ;
#4111=CIRCLE ( 'NONE', #7308, 3.000000000000000444 ) ;
#4118=VECTOR ( 'NONE', #1594, 39.37007874015748854 ) ;
#4125=CARTESIAN_POINT ( 'NONE',  ( 2.124999999999999556, -1.679378605318059048, -1.679378605318041950 ) ) ;
#4126=LINE ( 'NONE', #8640, #7006 ) ;
#4130=AXIS2_PLACEMENT_3D ( 'NONE', #9732, #14458, #6215 ) ;
#4133=CYLINDRICAL_SURFACE ( 'NONE', #4513, 0.7849999999999993650 ) ;
#4136=CARTESIAN_POINT ( 'NONE',  ( 0.06299999999999994493, -1.679378605318048390, 1.679378605318054163 ) ) ;
#4138=CIRCLE ( 'NONE', #10002, 2.500000000000000000 ) ;
#4141=DIMENSIONAL_EXPONENTS ( 1.000000000000000000, 0.000000000000000000, 0.000000000000000000, 0.000000000000000000, 0.000000000000000000, 0.000000000000000000, 0.000000000000000000 ) ;
#4147=ADVANCED_FACE ( 'NONE', ( #136 ), #8741, .F. ) ;
#4148=CIRCLE ( 'NONE', #13159, 2.500000000000000000 ) ;
#4149=CARTESIAN_POINT ( 'NONE',  ( 2.774999999999999911, 1.679378605318059048, 1.679378605318041506 ) ) ;
#4158=( NAMED_UNIT ( * ) PLANE_ANGLE_UNIT ( ) SI_UNIT ( $, .RADIAN. ) );
#4170=EDGE_LOOP ( 'NONE', ( #13287, #9721, #2751, #1462 ) ) ;
#4172=DIRECTION ( 'NONE',  ( 0.000000000000000000, 0.000000000000000000, 1.000000000000000000 ) ) ;
#4176=DIRECTION ( 'NONE',  ( 0.7071067811865471286, 8.659560562354939021E-17, 0.7071067811865479058 ) ) ;
#4181=VERTEX_POINT ( 'NONE', #10567 ) ;
#4183=EDGE_CURVE ( 'NONE', #7356, #524, #5135, .T. ) ;
#4186=LINE ( 'NONE', #7697, #7029 ) ;
#4187=CARTESIAN_POINT ( 'NONE',  ( 0.09500000000000431710, 1.679378605318035733, -1.304378605318064821 ) ) ;
#4196=VECTOR ( 'NONE', #5396, 39.37007874015748143 ) ;
#4202=ORIENTED_EDGE ( 'NONE', *, *, #144, .F. ) ;
#4203=CARTESIAN_POINT ( 'NONE',  ( 0.000000000000000000, 2.258248697627719244E-16, 1.812500000000000222 ) ) ;
#4205=ORIENTED_EDGE ( 'NONE', *, *, #1738, .T. ) ;
#4211=AXIS2_PLACEMENT_3D ( 'NONE', #6099, #10827, #10761 ) ;
#4213=PLANE ( 'NONE',  #8296 ) ;
#4217=ORIENTED_EDGE ( 'NONE', *, *, #9417, .T. ) ;
#4235=DIRECTION ( 'NONE',  ( 0.000000000000000000, 0.000000000000000000, -1.000000000000000000 ) ) ;
#4240=CARTESIAN_POINT ( 'NONE',  ( 0.06299999999999994493, 1.679378605318035733, -1.679378605318065487 ) ) ;
#4242=ORIENTED_EDGE ( 'NONE', *, *, #12833, .F. ) ;
#4243=ORIENTED_EDGE ( 'NONE', *, *, #805, .F. ) ;
#4244=CONICAL_SURFACE ( 'NONE', #59, 0.2624999999999852451, 0.7853981633974423948 ) ;
#4246=CONICAL_SURFACE ( 'NONE', #12777, 0.3750000000000007772, 0.7853981633974536081 ) ;
#4249=LINE ( 'NONE', #11430, #451 ) ;
#4258=ORIENTED_EDGE ( 'NONE', *, *, #889, .F. ) ;
#4267=DIRECTION ( 'NONE',  ( 0.7071067811865452413, 8.659560562354961208E-17, 0.7071067811865497932 ) ) ;
#4272=VECTOR ( 'NONE', #11891, 39.37007874015748143 ) ;
#4282=FACE_BOUND ( 'NONE', #3297, .T. ) ;
#4287=AXIS2_PLACEMENT_3D ( 'NONE', #5582, #12521, #8033 ) ;
#4288=AXIS2_PLACEMENT_3D ( 'NONE', #890, #12686, #1973 ) ;
#4294=DIRECTION ( 'NONE',  ( 0.000000000000000000, 0.000000000000000000, -1.000000000000000000 ) ) ;
#4302=AXIS2_PLACEMENT_3D ( 'NONE', #2416, #9464, #8329 ) ;
#4320=AXIS2_PLACEMENT_3D ( 'NONE', #2750, #572, #5427 ) ;
#4326=DIRECTION ( 'NONE',  ( 0.000000000000000000, 0.000000000000000000, 1.000000000000000000 ) ) ;
#4329=ADVANCED_FACE ( 'NONE', ( #4583 ), #3135, .F. ) ;
#4331=VERTEX_POINT ( 'NONE', #13673 ) ;
#4333=UNCERTAINTY_MEASURE_WITH_UNIT (LENGTH_MEASURE( 1.000000000000000082E-05 ), #14625, 'distance_accuracy_value', 'NONE');
#4336=DIRECTION ( 'NONE',  ( 0.000000000000000000, 0.000000000000000000, -1.000000000000000000 ) ) ;
#4344=AXIS2_PLACEMENT_3D ( 'NONE', #14581, #14355, #1647 ) ;
#4349=EDGE_LOOP ( 'NONE', ( #12450, #245, #130, #4624 ) ) ;
#4355=AXIS2_PLACEMENT_3D ( 'NONE', #14905, #1970, #5658 ) ;
#4357=FACE_OUTER_BOUND ( 'NONE', #1493, .T. ) ;
#4361=CIRCLE ( 'NONE', #6814, 0.3750000000000004996 ) ;
#4365=CARTESIAN_POINT ( 'NONE',  ( 2.774999999999999911, 0.000000000000000000, 0.000000000000000000 ) ) ;
#4366=ADVANCED_FACE ( 'NONE', ( #3206, #14752, #2119, #13817, #4282, #10246 ), #13590, .T. ) ;
#4376=CIRCLE ( 'NONE', #14141, 0.2624999999999997335 ) ;
#4379=ORIENTED_EDGE ( 'NONE', *, *, #11949, .F. ) ;
#4380=AXIS2_PLACEMENT_3D ( 'NONE', #14965, #12579, #953 ) ;
#4381=EDGE_CURVE ( 'NONE', #1062, #14092, #9001, .T. ) ;
#4384=ORIENTED_EDGE ( 'NONE', *, *, #3683, .F. ) ;
#4390=DIRECTION ( 'NONE',  ( 0.000000000000000000, 0.000000000000000000, -1.000000000000000000 ) ) ;
#4396=ORIENTED_EDGE ( 'NONE', *, *, #1117, .T. ) ;
#4397=CARTESIAN_POINT ( 'NONE',  ( 2.124999999999999556, 1.679378605318059048, 1.384878605318041744 ) ) ;
#4405=EDGE_CURVE ( 'NONE', #3668, #8487, #2203, .T. ) ;
#4406=CARTESIAN_POINT ( 'NONE',  ( 2.742999999999999883, -1.679378605318041950, 1.679378605318059048 ) ) ;
#4435=CARTESIAN_POINT ( 'NONE',  ( 2.774999999999999911, -1.575000000000027489, -1.574999999999989297 ) ) ;
#4450=VERTEX_POINT ( 'NONE', #8186 ) ;
#4451=DIRECTION ( 'NONE',  ( -1.000000000000000000, -0.000000000000000000, -0.000000000000000000 ) ) ;
#4462=CARTESIAN_POINT ( 'NONE',  ( 2.742999999999999883, -1.679378605318041950, 1.679378605318059048 ) ) ;
#4463=ORIENTED_EDGE ( 'NONE', *, *, #10825, .F. ) ;
#4465=DIRECTION ( 'NONE',  ( 0.000000000000000000, 1.224646799147354933E-16, 1.000000000000000000 ) ) ;
#4484=DIRECTION ( 'NONE',  ( -1.000000000000000000, -0.000000000000000000, -0.000000000000000000 ) ) ;
#4494=ADVANCED_FACE ( 'NONE', ( #14132 ), #10697, .F. ) ;
#4498=ORIENTED_EDGE ( 'NONE', *, *, #1639, .T. ) ;
#4501=ORIENTED_EDGE ( 'NONE', *, *, #6372, .T. ) ;
#4504=ORIENTED_EDGE ( 'NONE', *, *, #14877, .F. ) ;
#4509=VERTEX_POINT ( 'NONE', #9561 ) ;
#4511=CARTESIAN_POINT ( 'NONE',  ( 2.001999999999999780, 0.000000000000000000, 1.350000000000000089 ) ) ;
#4513=AXIS2_PLACEMENT_3D ( 'NONE', #6207, #508, #2907 ) ;
#4516=CARTESIAN_POINT ( 'NONE',  ( 0.09500000000000168032, 0.000000000000000000, 0.000000000000000000 ) ) ;
#4518=CARTESIAN_POINT ( 'NONE',  ( 0.09500000000000431710, -1.679378605318048390, 1.679378605318054163 ) ) ;
#4521=FACE_BOUND ( 'NONE', #13820, .T. ) ;
#4549=VECTOR ( 'NONE', #9113, 39.37007874015748854 ) ;
#4551=AXIS2_PLACEMENT_3D ( 'NONE', #10283, #9135, #4465 ) ;
#4553=LINE ( 'NONE', #9224, #14548 ) ;
#4562=EDGE_LOOP ( 'NONE', ( #13092, #6013 ) ) ;
#4566=ADVANCED_FACE ( 'NONE', ( #14492 ), #11135, .F. ) ;
#4570=AXIS2_PLACEMENT_3D ( 'NONE', #15035, #6016, #2337 ) ;
#4573=CIRCLE ( 'NONE', #13334, 1.000000000000000222 ) ;
#4578=AXIS2_PLACEMENT_3D ( 'NONE', #12045, #5093, #12197 ) ;
#4583=FACE_OUTER_BOUND ( 'NONE', #12959, .T. ) ;
#4588=CARTESIAN_POINT ( 'NONE',  ( 2.774999999999999911, -3.360000000000000320, 0.9799999999999999822 ) ) ;
#4601=PLANE ( 'NONE',  #5529 ) ;
#4613=VECTOR ( 'NONE', #13176, 39.37007874015748143 ) ;
#4615=DIRECTION ( 'NONE',  ( -1.000000000000000000, -0.000000000000000000, -0.000000000000000000 ) ) ;
#4622=VECTOR ( 'NONE', #8416, 39.37007874015748143 ) ;
#4624=ORIENTED_EDGE ( 'NONE', *, *, #831, .F. ) ;
#4625=CARTESIAN_POINT ( 'NONE',  ( 0.6500000000000001332, -1.679378605318048390, 2.086378605318058632 ) ) ;
#4628=LINE ( 'NONE', #11811, #7237 ) ;
#4638=VECTOR ( 'NONE', #14016, 39.37007874015748143 ) ;
#4655=ORIENTED_EDGE ( 'NONE', *, *, #9452, .T. ) ;
#4664=ORIENTED_EDGE ( 'NONE', *, *, #7466, .T. ) ;
#4666=CYLINDRICAL_SURFACE ( 'NONE', #8526, 1.000000000000000000 ) ;
#4669=ADVANCED_FACE ( 'NONE', ( #8560 ), #13833, .T. ) ;
#4673=FACE_OUTER_BOUND ( 'NONE', #6906, .T. ) ;
#4674=CARTESIAN_POINT ( 'NONE',  ( 2.774999999999999911, 1.679378605318059048, 1.941878605318041240 ) ) ;
#4675=DIRECTION ( 'NONE',  ( 1.000000000000000000, 0.000000000000000000, 0.000000000000000000 ) ) ;
#4681=ORIENTED_EDGE ( 'NONE', *, *, #11288, .F. ) ;
#4687=CIRCLE ( 'NONE', #740, 1.000000000000000000 ) ;
#4688=DIRECTION ( 'NONE',  ( 0.000000000000000000, 0.000000000000000000, -1.000000000000000000 ) ) ;
#4697=VERTEX_POINT ( 'NONE', #12279 ) ;
#4701=FACE_OUTER_BOUND ( 'NONE', #3430, .T. ) ;
#4702=ORIENTED_EDGE ( 'NONE', *, *, #5294, .F. ) ;
#4708=AXIS2_PLACEMENT_3D ( 'NONE', #75, #8376, #1305 ) ;
#4710=ORIENTED_EDGE ( 'NONE', *, *, #12531, .F. ) ;
#4714=DIRECTION ( 'NONE',  ( -1.000000000000000000, -0.000000000000000000, -0.000000000000000000 ) ) ;
#4724=CIRCLE ( 'NONE', #9848, 1.350000000000000089 ) ;
#4731=DIRECTION ( 'NONE',  ( 0.000000000000000000, 0.000000000000000000, -1.000000000000000000 ) ) ;
#4737=VECTOR ( 'NONE', #8116, 39.37007874015748143 ) ;
#4738=DIRECTION ( 'NONE',  ( 0.000000000000000000, 0.000000000000000000, 1.000000000000000000 ) ) ;
#4740=CIRCLE ( 'NONE', #1047, 0.2944999999999998175 ) ;
#4744=LINE ( 'NONE', #12607, #10718 ) ;
#4746=FACE_OUTER_BOUND ( 'NONE', #9753, .T. ) ;
#4750=EDGE_CURVE ( 'NONE', #9866, #651, #4573, .T. ) ;
#4753=DIRECTION ( 'NONE',  ( 1.000000000000000000, 0.000000000000000000, 0.000000000000000000 ) ) ;
#4758=DIRECTION ( 'NONE',  ( 0.000000000000000000, 0.000000000000000000, 1.000000000000000000 ) ) ;
#4765=VERTEX_POINT ( 'NONE', #14960 ) ;
#4770=DIRECTION ( 'NONE',  ( 0.000000000000000000, 0.000000000000000000, 1.000000000000000000 ) ) ;
#4784=AXIS2_PLACEMENT_3D ( 'NONE', #5602, #4753, #11636 ) ;
#4785=EDGE_CURVE ( 'NONE', #4697, #14026, #1625, .T. ) ;
#4787=EDGE_LOOP ( 'NONE', ( #12800, #9284, #6358, #3094 ) ) ;
#4788=ORIENTED_EDGE ( 'NONE', *, *, #6376, .T. ) ;
#4791=FACE_BOUND ( 'NONE', #10377, .T. ) ;
#4794=AXIS2_PLACEMENT_3D ( 'NONE', #4125, #8003, #9075 ) ;
#4797=LINE ( 'NONE', #8395, #13133 ) ;
#4798=ORIENTED_EDGE ( 'NONE', *, *, #8710, .T. ) ;
#4808=EDGE_LOOP ( 'NONE', ( #10694, #7225, #12447, #10277 ) ) ;
#4818=ORIENTED_EDGE ( 'NONE', *, *, #11847, .T. ) ;
#4820=CARTESIAN_POINT ( 'NONE',  ( 2.774999999999999911, -2.359999999999984333, 1.575000000000016387 ) ) ;
#4826=CARTESIAN_POINT ( 'NONE',  ( 2.774999999999999911, 2.399999999999999911, -0.7000000000000009548 ) ) ;
#4831=CARTESIAN_POINT ( 'NONE',  ( 0.6180000000000012150, 3.673940397442060361E-16, -3.000000000000000444 ) ) ;
#4836=DIRECTION ( 'NONE',  ( 0.000000000000000000, 0.000000000000000000, 1.000000000000000000 ) ) ;
#4838=DIRECTION ( 'NONE',  ( 0.000000000000000000, 0.000000000000000000, 1.000000000000000000 ) ) ;
#4840=DIRECTION ( 'NONE',  ( -1.000000000000000000, 0.000000000000000000, 0.000000000000000000 ) ) ;
#4841=EDGE_CURVE ( 'NONE', #10348, #9682, #4186, .T. ) ;
#4843=CARTESIAN_POINT ( 'NONE',  ( 0.6500000000000001332, 0.000000000000000000, 0.000000000000000000 ) ) ;
#4847=ORIENTED_EDGE ( 'NONE', *, *, #12582, .F. ) ;
#4851=ORIENTED_EDGE ( 'NONE', *, *, #4841, .F. ) ;
#4855=VERTEX_POINT ( 'NONE', #10075 ) ;
#4863=AXIS2_PLACEMENT_3D ( 'NONE', #900, #5371, #4294 ) ;
#4868=AXIS2_PLACEMENT_3D ( 'NONE', #14001, #4615, #3617 ) ;
#4869=ORIENTED_EDGE ( 'NONE', *, *, #11050, .T. ) ;
#4874=FACE_BOUND ( 'NONE', #12312, .T. ) ;
#4879=DIRECTION ( 'NONE',  ( 0.000000000000000000, -1.000000000000000000, 0.000000000000000000 ) ) ;
#4883=DIRECTION ( 'NONE',  ( -1.000000000000000000, -0.000000000000000000, -0.000000000000000000 ) ) ;
#4887=AXIS2_PLACEMENT_3D ( 'NONE', #2262, #7781, #6944 ) ;
#4890=ORIENTED_EDGE ( 'NONE', *, *, #7005, .T. ) ;
#4894=LINE ( 'NONE', #1119, #5544 ) ;
#4922=EDGE_LOOP ( 'NONE', ( #4980, #2118, #10802, #10525 ) ) ;
#4923=LINE ( 'NONE', #9591, #12533 ) ;
#4926=CARTESIAN_POINT ( 'NONE',  ( 2.124999999999999556, -3.360000000000000320, 0.9799999999999999822 ) ) ;
#4928=FACE_OUTER_BOUND ( 'NONE', #1114, .T. ) ;
#4934=VERTEX_POINT ( 'NONE', #6940 ) ;
#4944=ORIENTED_EDGE ( 'NONE', *, *, #7673, .T. ) ;
#4946=DIRECTION ( 'NONE',  ( -1.000000000000000000, -0.000000000000000000, -0.000000000000000000 ) ) ;
#4950=DIRECTION ( 'NONE',  ( -1.000000000000000000, -0.000000000000000000, -0.000000000000000000 ) ) ;
#4951=DIRECTION ( 'NONE',  ( -1.000000000000000000, -0.000000000000000000, -0.000000000000000000 ) ) ;
#4961=DIRECTION ( 'NONE',  ( 0.000000000000000000, 0.000000000000000000, -1.000000000000000000 ) ) ;
#4963=ORIENTED_EDGE ( 'NONE', *, *, #1950, .F. ) ;
#4970=DIRECTION ( 'NONE',  ( 0.000000000000000000, 0.000000000000000000, -1.000000000000000000 ) ) ;
#4971=LINE ( 'NONE', #9705, #4622 ) ;
#4977=EDGE_CURVE ( 'NONE', #4021, #557, #3792, .T. ) ;
#4980=ORIENTED_EDGE ( 'NONE', *, *, #2452, .F. ) ;
#4989=DIRECTION ( 'NONE',  ( 1.000000000000000000, 0.000000000000000000, 0.000000000000000000 ) ) ;
#4994=DIRECTION ( 'NONE',  ( 0.000000000000000000, 0.000000000000000000, -1.000000000000000000 ) ) ;
#4997=EDGE_CURVE ( 'NONE', #539, #969, #1250, .T. ) ;
#5000=LINE ( 'NONE', #370, #3000 ) ;
#5008=ORIENTED_EDGE ( 'NONE', *, *, #11686, .T. ) ;
#5012=CARTESIAN_POINT ( 'NONE',  ( 0.09500000000000431710, -1.679378605318047946, -1.304378605318053053 ) ) ;
#5013=CIRCLE ( 'NONE', #7447, 0.05999999999999990757 ) ;
#5016=EDGE_LOOP ( 'NONE', ( #5463, #737, #118, #4463 ) ) ;
#5021=DIRECTION ( 'NONE',  ( 0.000000000000000000, 0.000000000000000000, 1.000000000000000000 ) ) ;
#5023=FACE_OUTER_BOUND ( 'NONE', #8009, .T. ) ;
#5026=AXIS2_PLACEMENT_3D ( 'NONE', #4843, #6141, #10728 ) ;
#5031=AXIS2_PLACEMENT_3D ( 'NONE', #9808, #14699, #14461 ) ;
#5033=FACE_OUTER_BOUND ( 'NONE', #10319, .T. ) ;
#5034=VERTEX_POINT ( 'NONE', #8679 ) ;
#5044=CYLINDRICAL_SURFACE ( 'NONE', #4344, 3.000000000000000444 ) ;
#5053=CARTESIAN_POINT ( 'NONE',  ( 2.001999999999999780, 1.653273178848927113E-16, -1.350000000000000089 ) ) ;
#5055=EDGE_LOOP ( 'NONE', ( #8111, #8265 ) ) ;
#5062=CARTESIAN_POINT ( 'NONE',  ( 0.000000000000000000, 0.000000000000000000, 0.000000000000000000 ) ) ;
#5067=VECTOR ( 'NONE', #13338, 39.37007874015748143 ) ;
#5070=ORIENTED_EDGE ( 'NONE', *, *, #3723, .F. ) ;
#5073=CARTESIAN_POINT ( 'NONE',  ( 0.06299999999999998657, 2.296825071800860970E-16, 1.875500000000000167 ) ) ;
#5085=DIRECTION ( 'NONE',  ( 0.000000000000000000, 0.000000000000000000, -1.000000000000000000 ) ) ;
#5087=AXIS2_PLACEMENT_3D ( 'NONE', #4406, #6625, #774 ) ;
#5093=DIRECTION ( 'NONE',  ( -1.000000000000000000, -0.000000000000000000, -0.000000000000000000 ) ) ;
#5103=CIRCLE ( 'NONE', #669, 0.3750000000000004996 ) ;
#5105=CIRCLE ( 'NONE', #14378, 0.3750000000000004996 ) ;
#5107=EDGE_LOOP ( 'NONE', ( #10858, #11620 ) ) ;
#5109=CIRCLE ( 'NONE', #14634, 0.4070000000000058016 ) ;
#5110=VERTEX_POINT ( 'NONE', #7393 ) ;
#5111=LINE ( 'NONE', #4025, #5067 ) ;
#5118=AXIS2_PLACEMENT_3D ( 'NONE', #14454, #2762, #6213 ) ;
#5124=EDGE_CURVE ( 'NONE', #5889, #2080, #11780, .T. ) ;
#5126=CARTESIAN_POINT ( 'NONE',  ( 2.124999999999999556, 3.360000000000000320, -0.9800000000000012035 ) ) ;
#5131=ORIENTED_EDGE ( 'NONE', *, *, #144, .T. ) ;
#5133=EDGE_CURVE ( 'NONE', #12982, #863, #11034, .T. ) ;
#5135=LINE ( 'NONE', #506, #10217 ) ;
#5136=SHAPE_REPRESENTATION_RELATIONSHIP ( 'NONE' , 'NONE' ,  #10912, #14565 ) ;
#5141=EDGE_CURVE ( 'NONE', #12434, #13095, #13326, .T. ) ;
#5149=CARTESIAN_POINT ( 'NONE',  ( 0.000000000000000000, 0.000000000000000000, 1.350000000000000089 ) ) ;
#5150=FACE_OUTER_BOUND ( 'NONE', #4349, .T. ) ;
#5151=VERTEX_POINT ( 'NONE', #3099 ) ;
#5153=ORIENTED_EDGE ( 'NONE', *, *, #4405, .T. ) ;
#5158=CARTESIAN_POINT ( 'NONE',  ( 2.774999999999999911, 0.9800000000000039790, 3.360000000000000320 ) ) ;
#5162=VERTEX_POINT ( 'NONE', #1857 ) ;
#5166=LINE ( 'NONE', #2567, #11665 ) ;
#5167=DIRECTION ( 'NONE',  ( 0.000000000000000000, 0.000000000000000000, -1.000000000000000000 ) ) ;
#5173=CONICAL_SURFACE ( 'NONE', #9593, 0.2944999999999845519, 0.7853981633974509435 ) ;
#5175=ORIENTED_EDGE ( 'NONE', *, *, #14705, .F. ) ;
#5179=CARTESIAN_POINT ( 'NONE',  ( 2.124999999999999556, 0.6999999999999599876, -2.400000000000011458 ) ) ;
#5184=CARTESIAN_POINT ( 'NONE',  ( 0.6179999999999965521, 1.679378605318059492, 2.054378605318042172 ) ) ;
#5185=PRODUCT ( 'Outlet Housing', 'Outlet Housing', '', ( #9773 ) ) ;
#5200=CARTESIAN_POINT ( 'NONE',  ( 0.6500000000000001332, 0.000000000000000000, 2.968000000000000860 ) ) ;
#5202=CARTESIAN_POINT ( 'NONE',  ( 0.09500000000000431710, 1.679378605318059492, 1.679378605318041506 ) ) ;
#5205=AXIS2_PLACEMENT_3D ( 'NONE', #1930, #9209, #8900 ) ;
#5208=EDGE_CURVE ( 'NONE', #6943, #13629, #11346, .T. ) ;
#5219=CARTESIAN_POINT ( 'NONE',  ( 0.09500000000000431710, 1.679378605318059492, 1.679378605318041506 ) ) ;
#5220=ORIENTED_EDGE ( 'NONE', *, *, #1360, .F. ) ;
#5223=VECTOR ( 'NONE', #1312, 39.37007874015748143 ) ;
#5229=AXIS2_PLACEMENT_3D ( 'NONE', #11164, #9951, #6507 ) ;
#5235=DIRECTION ( 'NONE',  ( 1.000000000000000000, 0.000000000000000000, 0.000000000000000000 ) ) ;
#5242=ORIENTED_EDGE ( 'NONE', *, *, #8611, .F. ) ;
#5244=AXIS2_PLACEMENT_3D ( 'NONE', #9175, #10173, #2205 ) ;
#5246=CARTESIAN_POINT ( 'NONE',  ( 2.124999999999999556, 1.575000000000016165, 2.359999999999999876 ) ) ;
#5250=FACE_OUTER_BOUND ( 'NONE', #3670, .T. ) ;
#5253=FACE_OUTER_BOUND ( 'NONE', #8727, .T. ) ;
#5255=ADVANCED_FACE ( 'NONE', ( #3306 ), #5173, .F. ) ;
#5258=AXIS2_PLACEMENT_3D ( 'NONE', #7374, #1385, #2549 ) ;
#5266=EDGE_LOOP ( 'NONE', ( #6540, #2474, #2550, #11859 ) ) ;
#5273=DIRECTION ( 'NONE',  ( 0.000000000000000000, 0.000000000000000000, -1.000000000000000000 ) ) ;
#5277=CARTESIAN_POINT ( 'NONE',  ( 0.6500000000000001332, 1.679378605318035733, -2.086378605318070178 ) ) ;
#5279=VECTOR ( 'NONE', #7208, 39.37007874015748143 ) ;
#5286=DIRECTION ( 'NONE',  ( -1.000000000000000000, -0.000000000000000000, -0.000000000000000000 ) ) ;
#5292=ORIENTED_EDGE ( 'NONE', *, *, #12074, .F. ) ;
#5294=EDGE_CURVE ( 'NONE', #10348, #5886, #10068, .T. ) ;
#5301=ORIENTED_EDGE ( 'NONE', *, *, #3432, .T. ) ;
#5311=EDGE_LOOP ( 'NONE', ( #11465, #13743, #9308, #9477 ) ) ;
#5315=VECTOR ( 'NONE', #5336, 39.37007874015748143 ) ;
#5322=AXIS2_PLACEMENT_3D ( 'NONE', #7623, #3118, #8929 ) ;
#5327=EDGE_LOOP ( 'NONE', ( #13816, #14051 ) ) ;
#5336=DIRECTION ( 'NONE',  ( 0.000000000000000000, 4.591341165822166182E-16, 1.000000000000000000 ) ) ;
#5342=CIRCLE ( 'NONE', #13638, 0.3750000000000007772 ) ;
#5351=ORIENTED_EDGE ( 'NONE', *, *, #1693, .F. ) ;
#5353=ORIENTED_EDGE ( 'NONE', *, *, #1631, .F. ) ;
#5354=CIRCLE ( 'NONE', #5118, 0.7849999999999998090 ) ;
#5362=LINE ( 'NONE', #580, #6819 ) ;
#5371=DIRECTION ( 'NONE',  ( -1.000000000000000000, -0.000000000000000000, -0.000000000000000000 ) ) ;
#5372=DIRECTION ( 'NONE',  ( 1.000000000000000000, 0.000000000000000000, 0.000000000000000000 ) ) ;
#5373=CARTESIAN_POINT ( 'NONE',  ( 0.6179999999999965521, -1.679378605318047946, -2.054378605318054163 ) ) ;
#5377=CARTESIAN_POINT ( 'NONE',  ( 2.774999999999999911, 1.575000000000000178, -2.360000000000016751 ) ) ;
#5386=ORIENTED_EDGE ( 'NONE', *, *, #3906, .F. ) ;
#5391=ORIENTED_EDGE ( 'NONE', *, *, #11125, .F. ) ;
#5394=VERTEX_POINT ( 'NONE', #7179 ) ;
#5395=CARTESIAN_POINT ( 'NONE',  ( 1.375000000000000000, 0.000000000000000000, 1.350000000000000089 ) ) ;
#5396=DIRECTION ( 'NONE',  ( -1.000000000000000000, -0.000000000000000000, -0.000000000000000000 ) ) ;
#5397=CARTESIAN_POINT ( 'NONE',  ( 0.1250000000000009992, 0.000000000000000000, 0.000000000000000000 ) ) ;
#5399=ORIENTED_EDGE ( 'NONE', *, *, #14306, .T. ) ;
#5400=ADVANCED_FACE ( 'NONE', ( #12815 ), #9396, .F. ) ;
#5407=AXIS2_PLACEMENT_3D ( 'NONE', #13785, #14951, #7997 ) ;
#5410=CARTESIAN_POINT ( 'NONE',  ( 2.124999999999999556, 3.360000000000016751, 0.9799999999999461364 ) ) ;
#5415=LINE ( 'NONE', #13574, #12893 ) ;
#5416=DIRECTION ( 'NONE',  ( 0.000000000000000000, 0.000000000000000000, -1.000000000000000000 ) ) ;
#5425=VERTEX_POINT ( 'NONE', #14037 ) ;
#5427=DIRECTION ( 'NONE',  ( 0.000000000000000000, 0.000000000000000000, -1.000000000000000000 ) ) ;
#5429=ORIENTED_EDGE ( 'NONE', *, *, #12903, .T. ) ;
#5431=DIRECTION ( 'NONE',  ( 0.000000000000000000, 0.000000000000000000, -1.000000000000000000 ) ) ;
#5433=ORIENTED_EDGE ( 'NONE', *, *, #1360, .T. ) ;
#5435=CARTESIAN_POINT ( 'NONE',  ( 0.6179999999999965521, 1.679378605318059492, 2.054378605318042172 ) ) ;
#5441=VERTEX_POINT ( 'NONE', #12739 ) ;
#5453=DIRECTION ( 'NONE',  ( 0.000000000000000000, 0.000000000000000000, -1.000000000000000000 ) ) ;
#5460=CARTESIAN_POINT ( 'NONE',  ( 0.6500000000000001332, -1.679378605318047946, -2.086378605318057744 ) ) ;
#5463=ORIENTED_EDGE ( 'NONE', *, *, #13258, .F. ) ;
#5464=ORIENTED_EDGE ( 'NONE', *, *, #4785, .F. ) ;
#5467=FACE_OUTER_BOUND ( 'NONE', #6584, .T. ) ;
#5471=DIRECTION ( 'NONE',  ( 0.000000000000000000, 0.000000000000000000, 1.000000000000000000 ) ) ;
#5472=CARTESIAN_POINT ( 'NONE',  ( 2.774999999999999911, 0.000000000000000000, 2.500000000000000444 ) ) ;
#5474=EDGE_LOOP ( 'NONE', ( #8915, #7564, #6800, #6958 ) ) ;
#5481=DIRECTION ( 'NONE',  ( -1.000000000000000000, -0.000000000000000000, -0.000000000000000000 ) ) ;
#5486=CARTESIAN_POINT ( 'NONE',  ( 2.124999999999999556, 1.679378605318042395, -1.973878605318058588 ) ) ;
#5504=DIRECTION ( 'NONE',  ( -0.7071067811865479058, 0.000000000000000000, 0.7071067811865471286 ) ) ;
#5505=DIRECTION ( 'NONE',  ( 0.000000000000000000, 0.000000000000000000, 1.000000000000000000 ) ) ;
#5510=AXIS2_PLACEMENT_3D ( 'NONE', #15096, #6002, #10516 ) ;
#5517=DIRECTION ( 'NONE',  ( 0.7071067811865460184, 0.000000000000000000, -0.7071067811865490160 ) ) ;
#5524=VECTOR ( 'NONE', #14415, 39.37007874015748854 ) ;
#5527=ORIENTED_EDGE ( 'NONE', *, *, #2964, .T. ) ;
#5529=AXIS2_PLACEMENT_3D ( 'NONE', #14845, #13610, #7886 ) ;
#5533=AXIS2_PLACEMENT_3D ( 'NONE', #10441, #87, #6007 ) ;
#5534=CIRCLE ( 'NONE', #2843, 2.968000000000000860 ) ;
#5535=ORIENTED_EDGE ( 'NONE', *, *, #1083, .T. ) ;
#5537=DIRECTION ( 'NONE',  ( -1.000000000000000000, -0.000000000000000000, -0.000000000000000000 ) ) ;
#5538=CARTESIAN_POINT ( 'NONE',  ( 2.774999999999999911, -0.9799999999999436939, 2.360000000000016307 ) ) ;
#5544=VECTOR ( 'NONE', #5806, 39.37007874015748143 ) ;
#5573=VERTEX_POINT ( 'NONE', #2728 ) ;
#5574=CONICAL_SURFACE ( 'NONE', #9237, 0.3750000000000004996, 0.7853981633974621568 ) ;
#5582=CARTESIAN_POINT ( 'NONE',  ( 2.124999999999999556, -1.575000000000027489, -1.574999999999989297 ) ) ;
#5594=DIRECTION ( 'NONE',  ( 0.000000000000000000, 0.000000000000000000, -1.000000000000000000 ) ) ;
#5595=AXIS2_PLACEMENT_3D ( 'NONE', #13007, #6291, #4994 ) ;
#5602=CARTESIAN_POINT ( 'NONE',  ( 0.6179999999999965521, -1.679378605318047946, -1.679378605318053497 ) ) ;
#5612=ADVANCED_FACE ( 'NONE', ( #11148 ), #875, .F. ) ;
#5621=CARTESIAN_POINT ( 'NONE',  ( 2.743000000000000327, 1.679378605318042395, -1.416878605318059314 ) ) ;
#5622=ORIENTED_EDGE ( 'NONE', *, *, #468, .F. ) ;
#5623=DIRECTION ( 'NONE',  ( 0.000000000000000000, 0.000000000000000000, 1.000000000000000000 ) ) ;
#5633=ADVANCED_FACE ( 'NONE', ( #4928 ), #153, .F. ) ;
#5636=ORIENTED_EDGE ( 'NONE', *, *, #11972, .T. ) ;
#5644=ORIENTED_EDGE ( 'NONE', *, *, #14592, .F. ) ;
#5653=VERTEX_POINT ( 'NONE', #2475 ) ;
#5654=ORIENTED_EDGE ( 'NONE', *, *, #5767, .T. ) ;
#5658=DIRECTION ( 'NONE',  ( 0.000000000000000000, 0.000000000000000000, -1.000000000000000000 ) ) ;
#5666=CARTESIAN_POINT ( 'NONE',  ( 0.6179999999999965521, 1.679378605318059492, 1.679378605318041506 ) ) ;
#5672=VECTOR ( 'NONE', #11045, 39.37007874015748143 ) ;
#5675=VERTEX_POINT ( 'NONE', #1308 ) ;
#5676=ORIENTED_EDGE ( 'NONE', *, *, #9360, .T. ) ;
#5678=EDGE_LOOP ( 'NONE', ( #10987, #7748, #7757, #12865 ) ) ;
#5682=EDGE_CURVE ( 'NONE', #13454, #4934, #4687, .T. ) ;
#5701=DIRECTION ( 'NONE',  ( -1.000000000000000000, -0.000000000000000000, -0.000000000000000000 ) ) ;
#5708=EDGE_CURVE ( 'NONE', #4450, #14996, #10297, .T. ) ;
#5717=DIRECTION ( 'NONE',  ( -0.7071067811865441310, 8.659560562354974766E-17, -0.7071067811865509034 ) ) ;
#5743=DIRECTION ( 'NONE',  ( 1.000000000000000000, 0.000000000000000000, 0.000000000000000000 ) ) ;
#5757=LINE ( 'NONE', #13621, #8013 ) ;
#5758=CARTESIAN_POINT ( 'NONE',  ( 2.774999999999999911, 2.400000000000010569, 0.6999999999999612088 ) ) ;
#5767=EDGE_CURVE ( 'NONE', #13629, #11914, #14864, .T. ) ;
#5768=CARTESIAN_POINT ( 'NONE',  ( 0.6500000000000001332, -1.679378605318048390, 1.272378605318049249 ) ) ;
#5771=PLANE ( 'NONE',  #5510 ) ;
#5772=AXIS2_PLACEMENT_3D ( 'NONE', #8363, #7057, #13991 ) ;
#5774=CIRCLE ( 'NONE', #14313, 0.4070000000000058016 ) ;
#5777=DIRECTION ( 'NONE',  ( -1.000000000000000000, -0.000000000000000000, -0.000000000000000000 ) ) ;
#5778=CARTESIAN_POINT ( 'NONE',  ( 0.06299999999999994493, -1.679378605318047946, -1.679378605318053497 ) ) ;
#5779=AXIS2_PLACEMENT_3D ( 'NONE', #14129, #13966, #4731 ) ;
#5781=EDGE_CURVE ( 'NONE', #3137, #947, #10053, .T. ) ;
#5790=EDGE_LOOP ( 'NONE', ( #8170, #14456 ) ) ;
#5802=PLANE ( 'NONE',  #11569 ) ;
#5806=DIRECTION ( 'NONE',  ( -0.7071067811865400232, 8.659560562355026535E-17, -0.7071067811865551223 ) ) ;
#5812=EDGE_LOOP ( 'NONE', ( #8391, #13291, #1389, #4205 ) ) ;
#5813=LINE ( 'NONE', #12601, #11414 ) ;
#5822=DIRECTION ( 'NONE',  ( 0.000000000000000000, 0.000000000000000000, -1.000000000000000000 ) ) ;
#5825=DIRECTION ( 'NONE',  ( 0.000000000000000000, 0.000000000000000000, -1.000000000000000000 ) ) ;
#5829=CARTESIAN_POINT ( 'NONE',  ( 0.1250000000000009992, 0.000000000000000000, 0.000000000000000000 ) ) ;
#5841=AXIS2_PLACEMENT_3D ( 'NONE', #13311, #14776, #3167 ) ;
#5846=AXIS2_PLACEMENT_3D ( 'NONE', #6296, #13376, #10954 ) ;
#5851=CIRCLE ( 'NONE', #10971, 1.875000000000000000 ) ;
#5863=AXIS2_PLACEMENT_3D ( 'NONE', #10570, #15080, #3379 ) ;
#5865=ORIENTED_EDGE ( 'NONE', *, *, #11018, .T. ) ;
#5869=ORIENTED_EDGE ( 'NONE', *, *, #2773, .T. ) ;
#5873=CARTESIAN_POINT ( 'NONE',  ( 2.774999999999999911, 0.000000000000000000, 0.000000000000000000 ) ) ;
#5878=EDGE_CURVE ( 'NONE', #557, #2828, #14937, .T. ) ;
#5880=ADVANCED_FACE ( 'NONE', ( #8474 ), #999, .F. ) ;
#5882=DIRECTION ( 'NONE',  ( 0.000000000000000000, 0.000000000000000000, -1.000000000000000000 ) ) ;
#5886=VERTEX_POINT ( 'NONE', #4098 ) ;
#5889=VERTEX_POINT ( 'NONE', #4019 ) ;
#5892=DIRECTION ( 'NONE',  ( -1.000000000000000000, -0.000000000000000000, -0.000000000000000000 ) ) ;
#5897=CARTESIAN_POINT ( 'NONE',  ( 2.774999999999999911, 0.000000000000000000, 2.500000000000000444 ) ) ;
#5905=ORIENTED_EDGE ( 'NONE', *, *, #5781, .T. ) ;
#5906=DIRECTION ( 'NONE',  ( 0.000000000000000000, 0.000000000000000000, 1.000000000000000000 ) ) ;
#5915=LINE ( 'NONE', #9588, #13535 ) ;
#5921=DIRECTION ( 'NONE',  ( 0.000000000000000000, 0.000000000000000000, 1.000000000000000000 ) ) ;
#5924=ORIENTED_EDGE ( 'NONE', *, *, #7838, .T. ) ;
#5930=CARTESIAN_POINT ( 'NONE',  ( 0.09500000000000431710, -1.679378605318048390, 1.679378605318054163 ) ) ;
#5931=DIRECTION ( 'NONE',  ( 0.000000000000000000, 0.000000000000000000, -1.000000000000000000 ) ) ;
#5936=DIRECTION ( 'NONE',  ( 0.000000000000000000, 0.000000000000000000, 1.000000000000000000 ) ) ;
#5940=DIRECTION ( 'NONE',  ( -1.000000000000000000, -0.000000000000000000, -0.000000000000000000 ) ) ;
#5942=EDGE_CURVE ( 'NONE', #1772, #11127, #12722, .T. ) ;
#5951=ORIENTED_EDGE ( 'NONE', *, *, #2880, .T. ) ;
#5964=DIRECTION ( 'NONE',  ( -1.000000000000000000, -0.000000000000000000, -0.000000000000000000 ) ) ;
#5968=CARTESIAN_POINT ( 'NONE',  ( 1.375000000000000000, 0.000000000000000000, 0.000000000000000000 ) ) ;
#5976=ORIENTED_EDGE ( 'NONE', *, *, #8629, .T. ) ;
#5984=CIRCLE ( 'NONE', #2561, 0.3750000000000004996 ) ;
#5986=CARTESIAN_POINT ( 'NONE',  ( 2.775039370078740131, -1.679378605318048390, 1.679378605318054163 ) ) ;
#5988=EDGE_CURVE ( 'NONE', #4934, #6363, #4923, .T. ) ;
#5997=CARTESIAN_POINT ( 'NONE',  ( 0.000000000000000000, 0.000000000000000000, -1.812500000000000222 ) ) ;
#6002=DIRECTION ( 'NONE',  ( 0.000000000000000000, -1.000000000000000000, 4.591341165822166182E-16 ) ) ;
#6007=DIRECTION ( 'NONE',  ( 0.000000000000000000, 0.000000000000000000, 1.000000000000000000 ) ) ;
#6012=ORIENTED_EDGE ( 'NONE', *, *, #13463, .T. ) ;
#6013=ORIENTED_EDGE ( 'NONE', *, *, #1856, .T. ) ;
#6016=DIRECTION ( 'NONE',  ( -1.000000000000000000, -0.000000000000000000, -0.000000000000000000 ) ) ;
#6022=LINE ( 'NONE', #2727, #3405 ) ;
#6035=CONICAL_SURFACE ( 'NONE', #4320, 0.3750000000000004996, 0.7853981633974536081 ) ;
#6048=DIRECTION ( 'NONE',  ( 0.000000000000000000, 0.000000000000000000, -1.000000000000000000 ) ) ;
#6055=AXIS2_PLACEMENT_3D ( 'NONE', #13973, #7044, #4738 ) ;
#6056=FACE_OUTER_BOUND ( 'NONE', #13218, .T. ) ;
#6065=ADVANCED_FACE ( 'NONE', ( #14986 ), #13257, .F. ) ;
#6076=EDGE_CURVE ( 'NONE', #2531, #2396, #7047, .T. ) ;
#6087=CIRCLE ( 'NONE', #10959, 0.4070000000000044138 ) ;
#6093=ORIENTED_EDGE ( 'NONE', *, *, #14636, .T. ) ;
#6098=EDGE_CURVE ( 'NONE', #9866, #13738, #11625, .T. ) ;
#6099=CARTESIAN_POINT ( 'NONE',  ( 2.061999999999999833, 0.000000000000000000, 0.000000000000000000 ) ) ;
#6108=CARTESIAN_POINT ( 'NONE',  ( 2.124999999999999556, 1.574999999999994849, -1.575000000000022160 ) ) ;
#6116=EDGE_LOOP ( 'NONE', ( #11341, #11837, #3276, #8147 ) ) ;
#6121=CARTESIAN_POINT ( 'NONE',  ( 2.742999999999998995, -1.679378605318059048, -1.941878605318027251 ) ) ;
#6127=CARTESIAN_POINT ( 'NONE',  ( 2.061999999999999389, 0.000000000000000000, -1.409999999999999920 ) ) ;
#6140=EDGE_CURVE ( 'NONE', #14179, #6889, #8638, .T. ) ;
#6141=DIRECTION ( 'NONE',  ( 1.000000000000000000, 0.000000000000000000, 0.000000000000000000 ) ) ;
#6146=CARTESIAN_POINT ( 'NONE',  ( 2.774999999999999911, 1.575000000000000178, -2.360000000000016751 ) ) ;
#6159=CARTESIAN_POINT ( 'NONE',  ( 0.09500000000000431710, 1.679378605318059492, 2.054378605318042172 ) ) ;
#6163=EDGE_LOOP ( 'NONE', ( #10676, #11733, #4963, #6262 ) ) ;
#6169=CARTESIAN_POINT ( 'NONE',  ( 2.001999999999999780, 0.000000000000000000, 0.000000000000000000 ) ) ;
#6206=LENGTH_MEASURE_WITH_UNIT ( LENGTH_MEASURE( 0.02539999999999999897 ), #6361 );
#6207=CARTESIAN_POINT ( 'NONE',  ( 2.774999999999999911, 1.575000000000016609, 1.575000000000000178 ) ) ;
#6209=AXIS2_PLACEMENT_3D ( 'NONE', #3517, #7959, #14061 ) ;
#6213=DIRECTION ( 'NONE',  ( 0.000000000000000000, 0.000000000000000000, -1.000000000000000000 ) ) ;
#6215=DIRECTION ( 'NONE',  ( 0.000000000000000000, 0.000000000000000000, -1.000000000000000000 ) ) ;
#6217=CARTESIAN_POINT ( 'NONE',  ( 2.775039370078740131, -1.679378605318047946, -1.679378605318053497 ) ) ;
#6227=DIRECTION ( 'NONE',  ( -1.000000000000000000, -0.000000000000000000, -0.000000000000000000 ) ) ;
#6229=CARTESIAN_POINT ( 'NONE',  ( 2.774999999999999911, 2.360000000000015863, 1.574999999999999956 ) ) ;
#6232=VECTOR ( 'NONE', #8807, 39.37007874015748854 ) ;
#6236=VERTEX_POINT ( 'NONE', #10421 ) ;
#6237=DIRECTION ( 'NONE',  ( 0.000000000000000000, 0.000000000000000000, 1.000000000000000000 ) ) ;
#6241=CIRCLE ( 'NONE', #7951, 0.2944999999999998175 ) ;
#6242=DIRECTION ( 'NONE',  ( 0.000000000000000000, 0.000000000000000000, -1.000000000000000000 ) ) ;
#6250=ADVANCED_FACE ( 'NONE', ( #10439 ), #13751, .T. ) ;
#6251=VERTEX_POINT ( 'NONE', #6127 ) ;
#6262=ORIENTED_EDGE ( 'NONE', *, *, #7382, .F. ) ;
#6268=AXIS2_PLACEMENT_3D ( 'NONE', #2329, #8240, #7164 ) ;
#6281=ADVANCED_FACE ( 'NONE', ( #2211 ), #11073, .F. ) ;
#6287=DIMENSIONAL_EXPONENTS ( 1.000000000000000000, 0.000000000000000000, 0.000000000000000000, 0.000000000000000000, 0.000000000000000000, 0.000000000000000000, 0.000000000000000000 ) ;
#6291=DIRECTION ( 'NONE',  ( 1.000000000000000000, 0.000000000000000000, 0.000000000000000000 ) ) ;
#6293=DIRECTION ( 'NONE',  ( -0.7071067811865479058, 8.659560562354927928E-17, -0.7071067811865471286 ) ) ;
#6296=CARTESIAN_POINT ( 'NONE',  ( 0.000000000000000000, 1.812500000000000222, 0.000000000000000000 ) ) ;
#6300=ORIENTED_EDGE ( 'NONE', *, *, #7927, .T. ) ;
#6305=LINE ( 'NONE', #8744, #183 ) ;
#6311=AXIS2_PLACEMENT_3D ( 'NONE', #12933, #2382, #9506 ) ;
#6313=DIRECTION ( 'NONE',  ( -1.000000000000000000, -0.000000000000000000, -0.000000000000000000 ) ) ;
#6325=VECTOR ( 'NONE', #1657, 39.37007874015748854 ) ;
#6326=CIRCLE ( 'NONE', #11439, 1.000000000000000444 ) ;
#6332=VECTOR ( 'NONE', #8931, 39.37007874015748143 ) ;
#6336=PLANE ( 'NONE',  #13295 ) ;
#6343=LINE ( 'NONE', #8702, #12920 ) ;
#6348=EDGE_CURVE ( 'NONE', #11724, #733, #10180, .T. ) ;
#6358=ORIENTED_EDGE ( 'NONE', *, *, #14263, .F. ) ;
#6361=( LENGTH_UNIT ( ) NAMED_UNIT ( * ) SI_UNIT ( $, .METRE. ) );
#6363=VERTEX_POINT ( 'NONE', #6817 ) ;
#6370=FACE_OUTER_BOUND ( 'NONE', #3587, .T. ) ;
#6372=EDGE_CURVE ( 'NONE', #3706, #8947, #1794, .T. ) ;
#6376=EDGE_CURVE ( 'NONE', #6614, #11155, #2786, .T. ) ;
#6378=EDGE_LOOP ( 'NONE', ( #3883, #11772 ) ) ;
#6380=CARTESIAN_POINT ( 'NONE',  ( 2.650000000000001688, 0.000000000000000000, 0.000000000000000000 ) ) ;
#6386=EDGE_LOOP ( 'NONE', ( #13070, #9194, #8642, #12618 ) ) ;
#6392=CARTESIAN_POINT ( 'NONE',  ( 2.124999999999999556, 1.575000000000000178, -2.360000000000016751 ) ) ;
#6397=AXIS2_PLACEMENT_3D ( 'NONE', #10979, #4950, #5167 ) ;
#6398=ORIENTED_EDGE ( 'NONE', *, *, #14156, .F. ) ;
#6399=ORIENTED_EDGE ( 'NONE', *, *, #9452, .F. ) ;
#6401=LINE ( 'NONE', #5246, #636 ) ;
#6407=ORIENTED_EDGE ( 'NONE', *, *, #1982, .F. ) ;
#6419=ORIENTED_EDGE ( 'NONE', *, *, #14722, .T. ) ;
#6427=LINE ( 'NONE', #577, #1800 ) ;
#6435=ORIENTED_EDGE ( 'NONE', *, *, #1083, .F. ) ;
#6437=AXIS2_PLACEMENT_3D ( 'NONE', #4240, #3008, #4961 ) ;
#6441=LINE ( 'NONE', #10041, #8924 ) ;
#6448=CARTESIAN_POINT ( 'NONE',  ( 0.6179999999999965521, -1.679378605318047946, -1.304378605318053053 ) ) ;
#6449=ADVANCED_FACE ( 'NONE', ( #14410 ), #9643, .F. ) ;
#6452=EDGE_CURVE ( 'NONE', #4181, #4765, #11086, .T. ) ;
#6462=ORIENTED_EDGE ( 'NONE', *, *, #1918, .T. ) ;
#6468=EDGE_CURVE ( 'NONE', #8487, #3272, #3033, .T. ) ;
#6477=AXIS2_PLACEMENT_3D ( 'NONE', #1070, #10423, #4235 ) ;
#6481=ORIENTED_EDGE ( 'NONE', *, *, #6468, .T. ) ;
#6482=CARTESIAN_POINT ( 'NONE',  ( 2.124999999999999556, 2.359999999999999876, -1.575000000000016831 ) ) ;
#6487=EDGE_CURVE ( 'NONE', #4855, #3137, #13684, .T. ) ;
#6507=DIRECTION ( 'NONE',  ( 0.000000000000000000, 0.000000000000000000, -1.000000000000000000 ) ) ;
#6521=( LENGTH_UNIT ( ) NAMED_UNIT ( * ) SI_UNIT ( $, .METRE. ) );
#6525=EDGE_CURVE ( 'NONE', #10348, #14590, #13753, .T. ) ;
#6540=ORIENTED_EDGE ( 'NONE', *, *, #9380, .F. ) ;
#6541=FACE_OUTER_BOUND ( 'NONE', #6599, .T. ) ;
#6553=EDGE_CURVE ( 'NONE', #3706, #5573, #13911, .T. ) ;
#6556=DIRECTION ( 'NONE',  ( -0.000000000000000000, 4.591341165821852610E-16, -1.000000000000000000 ) ) ;
#6558=CARTESIAN_POINT ( 'NONE',  ( 2.774999999999999911, -2.360000000000000320, 1.575000000000016387 ) ) ;
#6565=CARTESIAN_POINT ( 'NONE',  ( 2.743000000000000771, 1.679378605318059048, 1.941878605318041240 ) ) ;
#6566=DIRECTION ( 'NONE',  ( 1.000000000000000000, 0.000000000000000000, 0.000000000000000000 ) ) ;
#6577=DIRECTION ( 'NONE',  ( -1.000000000000000000, 0.000000000000000000, 0.000000000000000000 ) ) ;
#6584=EDGE_LOOP ( 'NONE', ( #379, #3485, #578, #9295 ) ) ;
#6590=ORIENTED_EDGE ( 'NONE', *, *, #8313, .T. ) ;
#6591=CIRCLE ( 'NONE', #13171, 0.4070000000000055240 ) ;
#6599=EDGE_LOOP ( 'NONE', ( #8030, #4818, #8796, #7834 ) ) ;
#6609=CARTESIAN_POINT ( 'NONE',  ( 2.742999999999998995, -1.679378605318059048, -1.941878605318027251 ) ) ;
#6612=DIRECTION ( 'NONE',  ( 0.000000000000000000, 0.000000000000000000, 1.000000000000000000 ) ) ;
#6614=VERTEX_POINT ( 'NONE', #5053 ) ;
#6621=CARTESIAN_POINT ( 'NONE',  ( 0.09500000000000431710, -1.679378605318047946, -1.304378605318053053 ) ) ;
#6623=DIRECTION ( 'NONE',  ( -1.000000000000000000, -0.000000000000000000, -0.000000000000000000 ) ) ;
#6624=EDGE_CURVE ( 'NONE', #7356, #8150, #12071, .T. ) ;
#6625=DIRECTION ( 'NONE',  ( 1.000000000000000000, 0.000000000000000000, 0.000000000000000000 ) ) ;
#6627=ORIENTED_EDGE ( 'NONE', *, *, #7011, .T. ) ;
#6639=DIRECTION ( 'NONE',  ( 0.000000000000000000, 0.000000000000000000, -1.000000000000000000 ) ) ;
#6644=ADVANCED_FACE ( 'NONE', ( #10857 ), #10933, .F. ) ;
#6654=DIRECTION ( 'NONE',  ( -1.000000000000000000, -0.000000000000000000, -0.000000000000000000 ) ) ;
#6669=ORIENTED_EDGE ( 'NONE', *, *, #916, .F. ) ;
#6677=CARTESIAN_POINT ( 'NONE',  ( 2.124999999999999556, 0.000000000000000000, 0.000000000000000000 ) ) ;
#6691=DIRECTION ( 'NONE',  ( 1.000000000000000000, 0.000000000000000000, 0.000000000000000000 ) ) ;
#6695=AXIS2_PLACEMENT_3D ( 'NONE', #2449, #10782, #12816 ) ;
#6700=DIRECTION ( 'NONE',  ( -1.000000000000000000, -0.000000000000000000, -0.000000000000000000 ) ) ;
#6719=ORIENTED_EDGE ( 'NONE', *, *, #8746, .T. ) ;
#6724=CARTESIAN_POINT ( 'NONE',  ( 0.6500000000000001332, 0.000000000000000000, 0.000000000000000000 ) ) ;
#6730=CARTESIAN_POINT ( 'NONE',  ( 2.774999999999999911, 1.679378605318042395, -1.679378605318058604 ) ) ;
#6751=DIRECTION ( 'NONE',  ( 1.000000000000000000, 0.000000000000000000, 0.000000000000000000 ) ) ;
#6752=EDGE_LOOP ( 'NONE', ( #13215, #2206, #13012, #13717 ) ) ;
#6758=DIRECTION ( 'NONE',  ( -1.000000000000000000, -0.000000000000000000, 0.000000000000000000 ) ) ;
#6761=ORIENTED_EDGE ( 'NONE', *, *, #14209, .F. ) ;
#6763=FACE_OUTER_BOUND ( 'NONE', #12239, .T. ) ;
#6766=DIRECTION ( 'NONE',  ( -1.000000000000000000, -0.000000000000000000, -0.000000000000000000 ) ) ;
#6767=DIRECTION ( 'NONE',  ( 1.000000000000000000, 0.000000000000000000, 0.000000000000000000 ) ) ;
#6769=LINE ( 'NONE', #13706, #14272 ) ;
#6780=CIRCLE ( 'NONE', #7509, 3.000000000000000444 ) ;
#6788=ORIENTED_EDGE ( 'NONE', *, *, #6624, .T. ) ;
#6799=CIRCLE ( 'NONE', #8748, 0.2625000000000000111 ) ;
#6800=ORIENTED_EDGE ( 'NONE', *, *, #3989, .T. ) ;
#6803=ORIENTED_EDGE ( 'NONE', *, *, #8840, .F. ) ;
#6806=DIRECTION ( 'NONE',  ( 1.000000000000000000, 0.000000000000000000, 0.000000000000000000 ) ) ;
#6812=DIRECTION ( 'NONE',  ( -0.000000000000000000, -1.000000000000000000, -0.000000000000000000 ) ) ;
#6813=CARTESIAN_POINT ( 'NONE',  ( 2.156999999999999140, -1.679378605318041950, 1.416878605318058870 ) ) ;
#6814=AXIS2_PLACEMENT_3D ( 'NONE', #13451, #7960, #5594 ) ;
#6816=DIRECTION ( 'NONE',  ( 0.000000000000000000, 0.000000000000000000, 1.000000000000000000 ) ) ;
#6817=CARTESIAN_POINT ( 'NONE',  ( 2.124999999999999556, -2.399999999999999911, 0.6999999999999997335 ) ) ;
#6819=VECTOR ( 'NONE', #13293, 39.37007874015748143 ) ;
#6821=CARTESIAN_POINT ( 'NONE',  ( 0.09500000000000168032, 3.673940397442060361E-16, -3.000000000000000444 ) ) ;
#6822=DIRECTION ( 'NONE',  ( -1.000000000000000000, -0.000000000000000000, -0.000000000000000000 ) ) ;
#6827=VECTOR ( 'NONE', #1459, 39.37007874015748143 ) ;
#6829=CIRCLE ( 'NONE', #1417, 0.4070000000000046914 ) ;
#6831=CARTESIAN_POINT ( 'NONE',  ( 2.124999999999999556, 2.400000000000010569, 0.6999999999999612088 ) ) ;
#6839=DIRECTION ( 'NONE',  ( 0.000000000000000000, 0.000000000000000000, 1.000000000000000000 ) ) ;
#6840=CARTESIAN_POINT ( 'NONE',  ( 2.124999999999999556, -1.679378605318041950, 1.384878605318059064 ) ) ;
#6841=CARTESIAN_POINT ( 'NONE',  ( 2.774999999999999911, 1.679378605318059048, 1.973878605318040158 ) ) ;
#6846=CYLINDRICAL_SURFACE ( 'NONE', #1759, 0.3750000000000004996 ) ;
#6851=DIRECTION ( 'NONE',  ( 0.000000000000000000, 0.000000000000000000, 1.000000000000000000 ) ) ;
#6853=DIRECTION ( 'NONE',  ( 0.000000000000000000, 0.000000000000000000, -1.000000000000000000 ) ) ;
#6866=ORIENTED_EDGE ( 'NONE', *, *, #10727, .T. ) ;
#6867=DIRECTION ( 'NONE',  ( 0.7071067811865474617, 0.000000000000000000, -0.7071067811865474617 ) ) ;
#6886=EDGE_LOOP ( 'NONE', ( #6990, #12224, #12751, #11336 ) ) ;
#6887=CARTESIAN_POINT ( 'NONE',  ( 0.1250000000000009992, 0.000000000000000000, 1.000000000000000000 ) ) ;
#6889=VERTEX_POINT ( 'NONE', #14899 ) ;
#6894=DIRECTION ( 'NONE',  ( 1.000000000000000000, 0.000000000000000000, 0.000000000000000000 ) ) ;
#6896=DIRECTION ( 'NONE',  ( -1.000000000000000000, 0.000000000000000000, 0.000000000000000000 ) ) ;
#6897=CARTESIAN_POINT ( 'NONE',  ( 2.650000000000001688, 0.000000000000000000, 0.000000000000000000 ) ) ;
#6898=ADVANCED_FACE ( 'NONE', ( #7183 ), #8179, .T. ) ;
#6899=CARTESIAN_POINT ( 'NONE',  ( 2.124999999999999556, 1.679378605318042395, -1.679378605318058604 ) ) ;
#6901=DIRECTION ( 'NONE',  ( 0.000000000000000000, 0.000000000000000000, 1.000000000000000000 ) ) ;
#6904=FACE_OUTER_BOUND ( 'NONE', #14556, .T. ) ;
#6906=EDGE_LOOP ( 'NONE', ( #10580, #3298, #5301, #2738 ) ) ;
#6909=ORIENTED_EDGE ( 'NONE', *, *, #11483, .F. ) ;
#6912=DIRECTION ( 'NONE',  ( -1.000000000000000000, -0.000000000000000000, -0.000000000000000000 ) ) ;
#6916=EDGE_CURVE ( 'NONE', #11155, #6614, #4724, .T. ) ;
#6923=DIRECTION ( 'NONE',  ( 1.000000000000000000, 0.000000000000000000, 0.000000000000000000 ) ) ;
#6924=ORIENTED_EDGE ( 'NONE', *, *, #1694, .T. ) ;
#6928=ADVANCED_FACE ( 'NONE', ( #13963 ), #5802, .F. ) ;
#6940=CARTESIAN_POINT ( 'NONE',  ( 2.774999999999999911, -2.399999999999999911, 0.6999999999999997335 ) ) ;
#6941=FACE_BOUND ( 'NONE', #1039, .T. ) ;
#6942=CARTESIAN_POINT ( 'NONE',  ( 2.774999999999999911, 1.575000000000016165, 2.359999999999999876 ) ) ;
#6943=VERTEX_POINT ( 'NONE', #3583 ) ;
#6944=DIRECTION ( 'NONE',  ( 0.000000000000000000, 0.000000000000000000, -1.000000000000000000 ) ) ;
#6954=ORIENTED_EDGE ( 'NONE', *, *, #3518, .F. ) ;
#6958=ORIENTED_EDGE ( 'NONE', *, *, #4785, .T. ) ;
#6963=DIRECTION ( 'NONE',  ( -1.000000000000000000, -0.000000000000000000, -0.000000000000000000 ) ) ;
#6970=CIRCLE ( 'NONE', #6477, 0.9999999999999998890 ) ;
#6971=FACE_OUTER_BOUND ( 'NONE', #5812, .T. ) ;
#6974=CARTESIAN_POINT ( 'NONE',  ( 2.774999999999999911, -1.679378605318059048, -1.941878605318027251 ) ) ;
#6989=CARTESIAN_POINT ( 'NONE',  ( 2.774999999999999911, 2.359999999999994547, -1.575000000000016831 ) ) ;
#6990=ORIENTED_EDGE ( 'NONE', *, *, #4977, .T. ) ;
#6991=CIRCLE ( 'NONE', #5031, 0.3750000000000004996 ) ;
#6994=CONICAL_SURFACE ( 'NONE', #3557, 0.2625000000000000111, 0.7853981633974452814 ) ;
#7001=DIRECTION ( 'NONE',  ( -1.000000000000000000, -0.000000000000000000, -0.000000000000000000 ) ) ;
#7005=EDGE_CURVE ( 'NONE', #7063, #1193, #8158, .T. ) ;
#7006=VECTOR ( 'NONE', #1662, 39.37007874015748143 ) ;
#7009=CIRCLE ( 'NONE', #4794, 0.2944999999999845519 ) ;
#7010=DIRECTION ( 'NONE',  ( 0.000000000000000000, 0.000000000000000000, -1.000000000000000000 ) ) ;
#7011=EDGE_CURVE ( 'NONE', #524, #937, #14243, .T. ) ;
#7017=CARTESIAN_POINT ( 'NONE',  ( 2.742999999999999883, -1.679378605318041950, 1.679378605318059048 ) ) ;
#7018=ORIENTED_EDGE ( 'NONE', *, *, #14453, .F. ) ;
#7022=DIRECTION ( 'NONE',  ( 0.000000000000000000, 0.000000000000000000, 1.000000000000000000 ) ) ;
#7024=DIRECTION ( 'NONE',  ( 0.000000000000000000, 0.000000000000000000, -1.000000000000000000 ) ) ;
#7025=VECTOR ( 'NONE', #4714, 39.37007874015748143 ) ;
#7029=VECTOR ( 'NONE', #4484, 39.37007874015748143 ) ;
#7039=DIRECTION ( 'NONE',  ( 1.000000000000000000, 0.000000000000000000, 0.000000000000000000 ) ) ;
#7044=DIRECTION ( 'NONE',  ( -1.000000000000000000, 0.000000000000000000, 0.000000000000000000 ) ) ;
#7047=LINE ( 'NONE', #3286, #4737 ) ;
#7050=DIRECTION ( 'NONE',  ( -1.000000000000000000, -0.000000000000000000, -0.000000000000000000 ) ) ;
#7057=DIRECTION ( 'NONE',  ( 1.000000000000000000, 0.000000000000000000, 0.000000000000000000 ) ) ;
#7063=VERTEX_POINT ( 'NONE', #12335 ) ;
#7069=CIRCLE ( 'NONE', #10965, 1.494001693158433230 ) ;
#7070=LINE ( 'NONE', #5758, #1903 ) ;
#7071=CONICAL_SURFACE ( 'NONE', #8302, 0.2944999999999998175, 0.7853981633974520538 ) ;
#7073=AXIS2_PLACEMENT_3D ( 'NONE', #4926, #8225, #2623 ) ;
#7076=DIRECTION ( 'NONE',  ( 1.000000000000000000, 0.000000000000000000, 0.000000000000000000 ) ) ;
#7084=CARTESIAN_POINT ( 'NONE',  ( 1.375000000000000000, 0.000000000000000000, 0.000000000000000000 ) ) ;
#7095=EDGE_CURVE ( 'NONE', #12193, #8971, #4081, .T. ) ;
#7101=CARTESIAN_POINT ( 'NONE',  ( 2.774999999999999911, -0.6999999999999598765, 2.400000000000012346 ) ) ;
#7120=CARTESIAN_POINT ( 'NONE',  ( 0.09500000000000431710, 1.679378605318035733, -2.054378605318066153 ) ) ;
#7131=CARTESIAN_POINT ( 'NONE',  ( 0.06299999999999994493, 0.000000000000000000, 0.000000000000000000 ) ) ;
#7132=CARTESIAN_POINT ( 'NONE',  ( 2.774999999999999911, 3.360000000000000320, -0.9800000000000012035 ) ) ;
#7144=AXIS2_PLACEMENT_3D ( 'NONE', #3774, #13165, #4770 ) ;
#7145=DIRECTION ( 'NONE',  ( 0.000000000000000000, 0.000000000000000000, 1.000000000000000000 ) ) ;
#7146=ADVANCED_FACE ( 'NONE', ( #5033 ), #4244, .F. ) ;
#7159=DIRECTION ( 'NONE',  ( 0.000000000000000000, 0.000000000000000000, -1.000000000000000000 ) ) ;
#7161=DIRECTION ( 'NONE',  ( 0.000000000000000000, 0.000000000000000000, -1.000000000000000000 ) ) ;
#7164=DIRECTION ( 'NONE',  ( 0.000000000000000000, 0.000000000000000000, -1.000000000000000000 ) ) ;
#7167=EDGE_LOOP ( 'NONE', ( #10918, #9091, #8946, #12726 ) ) ;
#7174=VERTEX_POINT ( 'NONE', #5538 ) ;
#7179=CARTESIAN_POINT ( 'NONE',  ( 0.09500000000000431710, -1.679378605318047946, -2.054378605318054163 ) ) ;
#7183=FACE_OUTER_BOUND ( 'NONE', #10837, .T. ) ;
#7200=DIRECTION ( 'NONE',  ( 0.000000000000000000, 0.000000000000000000, 1.000000000000000000 ) ) ;
#7201=ADVANCED_FACE ( 'NONE', ( #13932 ), #2013, .F. ) ;
#7206=( GEOMETRIC_REPRESENTATION_CONTEXT ( 3 ) GLOBAL_UNCERTAINTY_ASSIGNED_CONTEXT ( ( #8328 ) ) GLOBAL_UNIT_ASSIGNED_CONTEXT ( ( #14300, #285, #10866 ) ) REPRESENTATION_CONTEXT ( 'NONE', 'WORKASPACE' ) );
#7208=DIRECTION ( 'NONE',  ( -0.000000000000000000, -9.182682331643740718E-16, 1.000000000000000000 ) ) ;
#7223=CARTESIAN_POINT ( 'NONE',  ( 0.09500000000000431710, 1.679378605318035733, -1.679378605318065487 ) ) ;
#7225=ORIENTED_EDGE ( 'NONE', *, *, #2104, .T. ) ;
#7226=FACE_OUTER_BOUND ( 'NONE', #14700, .T. ) ;
#7230=EDGE_CURVE ( 'NONE', #5886, #193, #1995, .T. ) ;
#7233=DIRECTION ( 'NONE',  ( -0.7071067811865455743, 0.000000000000000000, 0.7071067811865493491 ) ) ;
#7237=VECTOR ( 'NONE', #8079, 39.37007874015748143 ) ;
#7239=CARTESIAN_POINT ( 'NONE',  ( 2.774999999999999911, -1.679378605318041950, 1.416878605318058870 ) ) ;
#7246=DIRECTION ( 'NONE',  ( 0.000000000000000000, -1.000000000000000000, -4.591341165822158293E-16 ) ) ;
#7248=CIRCLE ( 'NONE', #2086, 0.4070000000000046914 ) ;
#7250=CARTESIAN_POINT ( 'NONE',  ( 2.774999999999999911, 0.9800000000000039790, 2.359999999999999876 ) ) ;
#7258=DIRECTION ( 'NONE',  ( -1.000000000000000000, -0.000000000000000000, -0.000000000000000000 ) ) ;
#7274=VECTOR ( 'NONE', #6556, 39.37007874015748143 ) ;
#7288=CARTESIAN_POINT ( 'NONE',  ( 2.124999999999999556, 0.9799999999999436939, -3.360000000000016751 ) ) ;
#7291=LINE ( 'NONE', #141, #4118 ) ;
#7308=AXIS2_PLACEMENT_3D ( 'NONE', #10344, #996, #1149 ) ;
#7309=AXIS2_PLACEMENT_3D ( 'NONE', #1698, #1395, #5085 ) ;
#7310=EDGE_CURVE ( 'NONE', #1160, #8873, #14008, .T. ) ;
#7325=DIRECTION ( 'NONE',  ( -1.000000000000000000, -0.000000000000000000, -0.000000000000000000 ) ) ;
#7328=LINE ( 'NONE', #30, #3653 ) ;
#7331=ADVANCED_FACE ( 'NONE', ( #10742 ), #2477, .F. ) ;
#7356=VERTEX_POINT ( 'NONE', #5997 ) ;
#7358=DIRECTION ( 'NONE',  ( 0.000000000000000000, 0.000000000000000000, 1.000000000000000000 ) ) ;
#7361=FACE_OUTER_BOUND ( 'NONE', #10495, .T. ) ;
#7372=ADVANCED_FACE ( 'NONE', ( #7226 ), #7, .T. ) ;
#7374=CARTESIAN_POINT ( 'NONE',  ( 2.774999999999999911, -0.9799999999999436939, 3.360000000000016751 ) ) ;
#7377=EDGE_LOOP ( 'NONE', ( #4847, #10943, #1774, #14240 ) ) ;
#7382=EDGE_CURVE ( 'NONE', #1793, #13688, #9523, .T. ) ;
#7383=VECTOR ( 'NONE', #3322, 39.37007874015748143 ) ;
#7387=VERTEX_POINT ( 'NONE', #14170 ) ;
#7393=CARTESIAN_POINT ( 'NONE',  ( 0.06299999999999994493, -1.679378605318047946, -1.272378605318047917 ) ) ;
#7401=VERTEX_POINT ( 'NONE', #9369 ) ;
#7402=ORIENTED_EDGE ( 'NONE', *, *, #5942, .F. ) ;
#7409=CARTESIAN_POINT ( 'NONE',  ( 0.000000000000000000, 0.000000000000000000, 0.000000000000000000 ) ) ;
#7416=DIRECTION ( 'NONE',  ( -1.000000000000000000, -0.000000000000000000, -0.000000000000000000 ) ) ;
#7423=AXIS2_PLACEMENT_3D ( 'NONE', #9670, #299, #13306 ) ;
#7427=ORIENTED_EDGE ( 'NONE', *, *, #10554, .F. ) ;
#7431=DIRECTION ( 'NONE',  ( -1.000000000000000000, -0.000000000000000000, -0.000000000000000000 ) ) ;
#7438=ORIENTED_EDGE ( 'NONE', *, *, #13062, .F. ) ;
#7447=AXIS2_PLACEMENT_3D ( 'NONE', #1404, #2644, #394 ) ;
#7452=VECTOR ( 'NONE', #13844, 39.37007874015748854 ) ;
#7453=ORIENTED_EDGE ( 'NONE', *, *, #11288, .T. ) ;
#7458=FACE_OUTER_BOUND ( 'NONE', #5016, .T. ) ;
#7461=VECTOR ( 'NONE', #968, 39.37007874015748143 ) ;
#7466=EDGE_CURVE ( 'NONE', #10168, #557, #7586, .T. ) ;
#7470=AXIS2_PLACEMENT_3D ( 'NONE', #7131, #9343, #15145 ) ;
#7474=CARTESIAN_POINT ( 'NONE',  ( 2.774999999999999911, -1.679378605318059048, -1.679378605318041950 ) ) ;
#7484=ADVANCED_FACE ( 'NONE', ( #5150 ), #2830, .F. ) ;
#7491=CARTESIAN_POINT ( 'NONE',  ( 0.000000000000000000, 0.000000000000000000, 0.000000000000000000 ) ) ;
#7495=ORIENTED_EDGE ( 'NONE', *, *, #4381, .F. ) ;
#7503=CARTESIAN_POINT ( 'NONE',  ( 2.124999999999999556, 1.679378605318059048, 1.973878605318041268 ) ) ;
#7509=AXIS2_PLACEMENT_3D ( 'NONE', #13129, #8415, #2671 ) ;
#7523=AXIS2_PLACEMENT_3D ( 'NONE', #12795, #11664, #460 ) ;
#7532=CIRCLE ( 'NONE', #1897, 0.4070000000000046914 ) ;
#7533=LINE ( 'NONE', #473, #8786 ) ;
#7538=EDGE_CURVE ( 'NONE', #10975, #11724, #6991, .T. ) ;
#7546=AXIS2_PLACEMENT_3D ( 'NONE', #4035, #9847, #6639 ) ;
#7556=ADVANCED_FACE ( 'NONE', ( #2925 ), #11129, .T. ) ;
#7557=VECTOR ( 'NONE', #5717, 39.37007874015748143 ) ;
#7560=CARTESIAN_POINT ( 'NONE',  ( 2.774999999999999911, -1.679378605318059048, -1.679378605318041950 ) ) ;
#7563=ORIENTED_EDGE ( 'NONE', *, *, #5141, .F. ) ;
#7564=ORIENTED_EDGE ( 'NONE', *, *, #9280, .F. ) ;
#7580=EDGE_LOOP ( 'NONE', ( #11559, #5433, #12075, #2139 ) ) ;
#7583=FACE_OUTER_BOUND ( 'NONE', #4808, .T. ) ;
#7586=LINE ( 'NONE', #5377, #11623 ) ;
#7589=ORIENTED_EDGE ( 'NONE', *, *, #3252, .T. ) ;
#7595=DIRECTION ( 'NONE',  ( -0.7071067811865376918, 8.659560562355053653E-17, -0.7071067811865573427 ) ) ;
#7608=DIRECTION ( 'NONE',  ( -0.000000000000000000, 0.000000000000000000, 1.000000000000000000 ) ) ;
#7610=ORIENTED_EDGE ( 'NONE', *, *, #8453, .T. ) ;
#7611=ORIENTED_EDGE ( 'NONE', *, *, #8686, .F. ) ;
#7612=VERTEX_POINT ( 'NONE', #6831 ) ;
#7623=CARTESIAN_POINT ( 'NONE',  ( 2.774999999999999911, 0.9799999999999436939, -3.360000000000016751 ) ) ;
#7625=LINE ( 'NONE', #3963, #9283 ) ;
#7626=PRODUCT_DEFINITION_SHAPE ( 'NONE', 'NONE',  #13772 ) ;
#7645=LINE ( 'NONE', #3055, #3313 ) ;
#7646=DIRECTION ( 'NONE',  ( -1.000000000000000000, -0.000000000000000000, -0.000000000000000000 ) ) ;
#7648=LINE ( 'NONE', #9729, #3060 ) ;
#7651=ORIENTED_EDGE ( 'NONE', *, *, #9887, .F. ) ;
#7655=DIRECTION ( 'NONE',  ( 1.000000000000000000, 0.000000000000000000, 0.000000000000000000 ) ) ;
#7665=CONICAL_SURFACE ( 'NONE', #7908, 0.2944999999999998175, 0.7853981633974530530 ) ;
#7670=VERTEX_POINT ( 'NONE', #10415 ) ;
#7673=EDGE_CURVE ( 'NONE', #9005, #11004, #9043, .T. ) ;
#7677=ORIENTED_EDGE ( 'NONE', *, *, #6098, .F. ) ;
#7685=AXIS2_PLACEMENT_3D ( 'NONE', #8836, #9065, #3242 ) ;
#7686=DIRECTION ( 'NONE',  ( -1.000000000000000000, -0.000000000000000000, -0.000000000000000000 ) ) ;
#7691=EDGE_LOOP ( 'NONE', ( #3592, #2261 ) ) ;
#7693=ORIENTED_EDGE ( 'NONE', *, *, #9491, .T. ) ;
#7697=CARTESIAN_POINT ( 'NONE',  ( 2.774999999999999911, 1.679378605318042395, -1.941878605318058115 ) ) ;
#7710=ADVANCED_FACE ( 'NONE', ( #9277, #13915, #7738, #4521, #2222, #6904 ), #4601, .F. ) ;
#7725=CIRCLE ( 'NONE', #371, 1.409999999999999920 ) ;
#7731=AXIS2_PLACEMENT_3D ( 'NONE', #6724, #9026, #8028 ) ;
#7738=FACE_BOUND ( 'NONE', #9025, .T. ) ;
#7739=EDGE_LOOP ( 'NONE', ( #3969, #5676 ) ) ;
#7746=DIRECTION ( 'NONE',  ( 1.000000000000000000, 0.000000000000000000, 0.000000000000000000 ) ) ;
#7748=ORIENTED_EDGE ( 'NONE', *, *, #9380, .T. ) ;
#7755=ORIENTED_EDGE ( 'NONE', *, *, #2103, .F. ) ;
#7757=ORIENTED_EDGE ( 'NONE', *, *, #2447, .T. ) ;
#7759=CONICAL_SURFACE ( 'NONE', #6055, 0.3750000000000004996, 0.7853981633974557175 ) ;
#7780=DIRECTION ( 'NONE',  ( -1.000000000000000000, -0.000000000000000000, -0.000000000000000000 ) ) ;
#7781=DIRECTION ( 'NONE',  ( 1.000000000000000000, 0.000000000000000000, 0.000000000000000000 ) ) ;
#7786=AXIS2_PLACEMENT_3D ( 'NONE', #3085, #9972, #4390 ) ;
#7794=ORIENTED_EDGE ( 'NONE', *, *, #6098, .T. ) ;
#7805=CIRCLE ( 'NONE', #4887, 0.7849999999999996980 ) ;
#7813=DIRECTION ( 'NONE',  ( 0.7071067811865501263, 0.000000000000000000, -0.7071067811865449082 ) ) ;
#7815=CYLINDRICAL_SURFACE ( 'NONE', #3807, 1.000000000000000222 ) ;
#7819=ORIENTED_EDGE ( 'NONE', *, *, #3518, .T. ) ;
#7820=ADVANCED_FACE ( 'NONE', ( #9502 ), #14067, .F. ) ;
#7825=ORIENTED_EDGE ( 'NONE', *, *, #1206, .T. ) ;
#7834=ORIENTED_EDGE ( 'NONE', *, *, #88, .F. ) ;
#7838=EDGE_CURVE ( 'NONE', #8947, #3706, #857, .T. ) ;
#7842=DIRECTION ( 'NONE',  ( 1.000000000000000000, 0.000000000000000000, 0.000000000000000000 ) ) ;
#7848=ORIENTED_EDGE ( 'NONE', *, *, #3855, .F. ) ;
#7849=EDGE_LOOP ( 'NONE', ( #11139, #4702, #13967, #12789 ) ) ;
#7870=CARTESIAN_POINT ( 'NONE',  ( 2.774999999999999911, 3.360000000000016751, 0.9799999999999461364 ) ) ;
#7872=CYLINDRICAL_SURFACE ( 'NONE', #10384, 1.350000000000000089 ) ;
#7875=DIRECTION ( 'NONE',  ( 0.000000000000000000, 0.000000000000000000, 1.000000000000000000 ) ) ;
#7886=DIRECTION ( 'NONE',  ( -0.000000000000000000, 0.000000000000000000, 1.000000000000000000 ) ) ;
#7888=ORIENTED_EDGE ( 'NONE', *, *, #1639, .F. ) ;
#7895=VECTOR ( 'NONE', #7258, 39.37007874015748143 ) ;
#7897=EDGE_LOOP ( 'NONE', ( #2442, #2928, #9938, #12480 ) ) ;
#7901=EDGE_LOOP ( 'NONE', ( #12700, #9002, #5391, #429 ) ) ;
#7906=VECTOR ( 'NONE', #15144, 39.37007874015748143 ) ;
#7908=AXIS2_PLACEMENT_3D ( 'NONE', #13015, #1079, #11741 ) ;
#7912=ORIENTED_EDGE ( 'NONE', *, *, #8407, .T. ) ;
#7920=ORIENTED_EDGE ( 'NONE', *, *, #11050, .F. ) ;
#7926=FACE_OUTER_BOUND ( 'NONE', #3953, .T. ) ;
#7927=EDGE_CURVE ( 'NONE', #13385, #9406, #4126, .T. ) ;
#7939=ORIENTED_EDGE ( 'NONE', *, *, #8665, .F. ) ;
#7945=DIRECTION ( 'NONE',  ( -1.000000000000000000, -0.000000000000000000, -0.000000000000000000 ) ) ;
#7946=CARTESIAN_POINT ( 'NONE',  ( 0.7100000000000001865, 0.000000000000000000, 0.000000000000000000 ) ) ;
#7947=ORIENTED_EDGE ( 'NONE', *, *, #8686, .T. ) ;
#7951=AXIS2_PLACEMENT_3D ( 'NONE', #3136, #13819, #11542 ) ;
#7952=CARTESIAN_POINT ( 'NONE',  ( 0.6180000000000012150, 0.000000000000000000, 0.000000000000000000 ) ) ;
#7959=DIRECTION ( 'NONE',  ( -1.000000000000000000, -0.000000000000000000, -0.000000000000000000 ) ) ;
#7960=DIRECTION ( 'NONE',  ( -1.000000000000000000, 0.000000000000000000, 0.000000000000000000 ) ) ;
#7963=VECTOR ( 'NONE', #15012, 39.37007874015748143 ) ;
#7968=AXIS2_PLACEMENT_3D ( 'NONE', #2676, #13134, #8568 ) ;
#7982=ORIENTED_EDGE ( 'NONE', *, *, #12031, .F. ) ;
#7989=CARTESIAN_POINT ( 'NONE',  ( 0.6500000000000001332, 0.000000000000000000, 0.000000000000000000 ) ) ;
#7994=LINE ( 'NONE', #5472, #3627 ) ;
#7996=AXIS2_PLACEMENT_3D ( 'NONE', #7474, #8559, #2953 ) ;
#7997=DIRECTION ( 'NONE',  ( 0.000000000000000000, 0.000000000000000000, -1.000000000000000000 ) ) ;
#8000=ORIENTED_EDGE ( 'NONE', *, *, #13641, .F. ) ;
#8003=DIRECTION ( 'NONE',  ( 1.000000000000000000, 0.000000000000000000, 0.000000000000000000 ) ) ;
#8004=EDGE_LOOP ( 'NONE', ( #942, #2390, #7819, #11176 ) ) ;
#8005=LINE ( 'NONE', #10372, #7025 ) ;
#8006=DIRECTION ( 'NONE',  ( 0.000000000000000000, 0.000000000000000000, -1.000000000000000000 ) ) ;
#8009=EDGE_LOOP ( 'NONE', ( #4243, #5636, #8688, #13471 ) ) ;
#8013=VECTOR ( 'NONE', #10342, 39.37007874015748143 ) ;
#8023=ORIENTED_EDGE ( 'NONE', *, *, #1300, .F. ) ;
#8024=CARTESIAN_POINT ( 'NONE',  ( 2.001999999999999780, 0.000000000000000000, 0.000000000000000000 ) ) ;
#8025=ORIENTED_EDGE ( 'NONE', *, *, #2141, .T. ) ;
#8026=CONICAL_SURFACE ( 'NONE', #7523, 0.2624999999999997335, 0.7853981633974479459 ) ;
#8028=DIRECTION ( 'NONE',  ( 0.000000000000000000, 0.000000000000000000, 1.000000000000000000 ) ) ;
#8029=ORIENTED_EDGE ( 'NONE', *, *, #14387, .F. ) ;
#8030=ORIENTED_EDGE ( 'NONE', *, *, #1694, .F. ) ;
#8033=DIRECTION ( 'NONE',  ( 0.000000000000000000, 0.000000000000000000, -1.000000000000000000 ) ) ;
#8038=EDGE_CURVE ( 'NONE', #2396, #13435, #8714, .T. ) ;
#8040=AXIS2_PLACEMENT_3D ( 'NONE', #11714, #2132, #13981 ) ;
#8042=CIRCLE ( 'NONE', #7073, 1.000000000000000000 ) ;
#8045=DIRECTION ( 'NONE',  ( 0.000000000000000000, 0.000000000000000000, -1.000000000000000000 ) ) ;
#8046=DIRECTION ( 'NONE',  ( -1.000000000000000000, -0.000000000000000000, -0.000000000000000000 ) ) ;
#8051=ADVANCED_FACE ( 'NONE', ( #11074 ), #6035, .F. ) ;
#8062=DIRECTION ( 'NONE',  ( 1.000000000000000000, 0.000000000000000000, 0.000000000000000000 ) ) ;
#8068=ORIENTED_EDGE ( 'NONE', *, *, #8454, .T. ) ;
#8070=CARTESIAN_POINT ( 'NONE',  ( 2.774999999999999911, 0.9799999999999438050, -2.360000000000016307 ) ) ;
#8075=EDGE_CURVE ( 'NONE', #13702, #8364, #142, .T. ) ;
#8077=CARTESIAN_POINT ( 'NONE',  ( 2.124999999999999556, -2.360000000000016751, -1.574999999999999956 ) ) ;
#8079=DIRECTION ( 'NONE',  ( -1.000000000000000000, -0.000000000000000000, -0.000000000000000000 ) ) ;
#8086=ORIENTED_EDGE ( 'NONE', *, *, #11769, .F. ) ;
#8087=EDGE_CURVE ( 'NONE', #1719, #5573, #12608, .T. ) ;
#8099=CARTESIAN_POINT ( 'NONE',  ( 2.124999999999999556, -1.679378605318059048, -1.679378605318041950 ) ) ;
#8102=DIRECTION ( 'NONE',  ( -1.000000000000000000, -0.000000000000000000, -0.000000000000000000 ) ) ;
#8105=CARTESIAN_POINT ( 'NONE',  ( 0.6975252985509352577, 0.000000000000000000, 1.494001693158432786 ) ) ;
#8111=ORIENTED_EDGE ( 'NONE', *, *, #160, .T. ) ;
#8116=DIRECTION ( 'NONE',  ( 0.000000000000000000, 1.000000000000000000, 4.591341165822158293E-16 ) ) ;
#8119=FACE_OUTER_BOUND ( 'NONE', #2684, .T. ) ;
#8122=EDGE_CURVE ( 'NONE', #11673, #11895, #11144, .T. ) ;
#8123=DIRECTION ( 'NONE',  ( -1.000000000000000000, -0.000000000000000000, -0.000000000000000000 ) ) ;
#8132=ORIENTED_EDGE ( 'NONE', *, *, #6916, .T. ) ;
#8147=ORIENTED_EDGE ( 'NONE', *, *, #8611, .T. ) ;
#8148=AXIS2_PLACEMENT_3D ( 'NONE', #2435, #11531, #5882 ) ;
#8150=VERTEX_POINT ( 'NONE', #4203 ) ;
#8152=FACE_OUTER_BOUND ( 'NONE', #6386, .T. ) ;
#8155=FACE_OUTER_BOUND ( 'NONE', #9996, .T. ) ;
#8158=CIRCLE ( 'NONE', #6437, 0.4070000000000058016 ) ;
#8161=ORIENTED_EDGE ( 'NONE', *, *, #3595, .F. ) ;
#8170=ORIENTED_EDGE ( 'NONE', *, *, #9557, .T. ) ;
#8179=CYLINDRICAL_SURFACE ( 'NONE', #14478, 2.499999999999999556 ) ;
#8184=EDGE_LOOP ( 'NONE', ( #10665, #8029, #2056, #11820 ) ) ;
#8186=CARTESIAN_POINT ( 'NONE',  ( 2.774999999999999911, 2.400000000000010569, 0.6999999999999612088 ) ) ;
#8197=VECTOR ( 'NONE', #14407, 39.37007874015748143 ) ;
#8201=LINE ( 'NONE', #11857, #931 ) ;
#8203=ORIENTED_EDGE ( 'NONE', *, *, #14099, .T. ) ;
#8214=CONICAL_SURFACE ( 'NONE', #8684, 0.2624999999999994560, 0.7853981633974446153 ) ;
#8216=EDGE_CURVE ( 'NONE', #5394, #3609, #4894, .T. ) ;
#8225=DIRECTION ( 'NONE',  ( -1.000000000000000000, -0.000000000000000000, 0.000000000000000000 ) ) ;
#8227=ORIENTED_EDGE ( 'NONE', *, *, #12495, .F. ) ;
#8240=DIRECTION ( 'NONE',  ( -1.000000000000000000, -0.000000000000000000, -0.000000000000000000 ) ) ;
#8241=CONICAL_SURFACE ( 'NONE', #5779, 0.3750000000000004996, 0.7853981633974514986 ) ;
#8252=ADVANCED_FACE ( 'NONE', ( #11840 ), #12362, .F. ) ;
#8265=ORIENTED_EDGE ( 'NONE', *, *, #1026, .T. ) ;
#8270=ADVANCED_FACE ( 'NONE', ( #11696 ), #8241, .F. ) ;
#8279=AXIS2_PLACEMENT_3D ( 'NONE', #14876, #1943, #9144 ) ;
#8289=AXIS2_PLACEMENT_3D ( 'NONE', #4516, #5743, #2373 ) ;
#8290=DIRECTION ( 'NONE',  ( -1.000000000000000000, -0.000000000000000000, -0.000000000000000000 ) ) ;
#8296=AXIS2_PLACEMENT_3D ( 'NONE', #12162, #8953, #2834 ) ;
#8302=AXIS2_PLACEMENT_3D ( 'NONE', #14437, #12991, #7200 ) ;
#8307=DIRECTION ( 'NONE',  ( -1.000000000000000000, -0.000000000000000000, -0.000000000000000000 ) ) ;
#8309=CIRCLE ( 'NONE', #8772, 1.409999999999999920 ) ;
#8312=ORIENTED_EDGE ( 'NONE', *, *, #7673, .F. ) ;
#8313=EDGE_CURVE ( 'NONE', #13454, #4101, #9253, .T. ) ;
#8320=ADVANCED_FACE ( 'NONE', ( #10695 ), #14566, .F. ) ;
#8323=VERTEX_POINT ( 'NONE', #1343 ) ;
#8326=ORIENTED_EDGE ( 'NONE', *, *, #14306, .F. ) ;
#8328=UNCERTAINTY_MEASURE_WITH_UNIT (LENGTH_MEASURE( 1.000000000000000082E-05 ), #14300, 'distance_accuracy_value', 'NONE');
#8329=DIRECTION ( 'NONE',  ( 0.000000000000000000, 0.000000000000000000, -1.000000000000000000 ) ) ;
#8335=LINE ( 'NONE', #12968, #11213 ) ;
#8345=DIRECTION ( 'NONE',  ( 0.000000000000000000, 0.000000000000000000, -1.000000000000000000 ) ) ;
#8346=ORIENTED_EDGE ( 'NONE', *, *, #14592, .T. ) ;
#8357=CARTESIAN_POINT ( 'NONE',  ( 0.09500000000000431710, -1.679378605318047946, -1.679378605318053497 ) ) ;
#8359=DIRECTION ( 'NONE',  ( 1.000000000000000000, 0.000000000000000000, 0.000000000000000000 ) ) ;
#8363=CARTESIAN_POINT ( 'NONE',  ( 2.742999999999998995, -1.679378605318059048, -1.679378605318041950 ) ) ;
#8364=VERTEX_POINT ( 'NONE', #7120 ) ;
#8369=ORIENTED_EDGE ( 'NONE', *, *, #14387, .T. ) ;
#8375=AXIS2_PLACEMENT_3D ( 'NONE', #14336, #2944, #5021 ) ;
#8376=DIRECTION ( 'NONE',  ( -1.000000000000000000, -0.000000000000000000, -0.000000000000000000 ) ) ;
#8377=DIRECTION ( 'NONE',  ( -1.000000000000000000, -0.000000000000000000, -0.000000000000000000 ) ) ;
#8379=CARTESIAN_POINT ( 'NONE',  ( 0.06299999999999994493, 3.634751699869342187E-16, 2.967999999999998639 ) ) ;
#8382=VERTEX_POINT ( 'NONE', #8105 ) ;
#8385=DIRECTION ( 'NONE',  ( -1.000000000000000000, 0.000000000000000000, 0.000000000000000000 ) ) ;
#8386=CARTESIAN_POINT ( 'NONE',  ( 2.124999999999999556, 0.000000000000000000, 0.000000000000000000 ) ) ;
#8389=EDGE_LOOP ( 'NONE', ( #11516, #1885, #4869, #5353 ) ) ;
#8391=ORIENTED_EDGE ( 'NONE', *, *, #1028, .F. ) ;
#8395=CARTESIAN_POINT ( 'NONE',  ( 2.774999999999999911, -2.360000000000000320, 1.575000000000016387 ) ) ;
#8402=EDGE_CURVE ( 'NONE', #11962, #11381, #8974, .T. ) ;
#8407=EDGE_CURVE ( 'NONE', #8947, #11381, #5111, .T. ) ;
#8408=ORIENTED_EDGE ( 'NONE', *, *, #14212, .F. ) ;
#8415=DIRECTION ( 'NONE',  ( -1.000000000000000000, -0.000000000000000000, -0.000000000000000000 ) ) ;
#8416=DIRECTION ( 'NONE',  ( -1.000000000000000000, -0.000000000000000000, -0.000000000000000000 ) ) ;
#8424=AXIS2_PLACEMENT_3D ( 'NONE', #5062, #7358, #1521 ) ;
#8440=DIRECTION ( 'NONE',  ( 0.000000000000000000, 0.000000000000000000, 1.000000000000000000 ) ) ;
#8444=DIRECTION ( 'NONE',  ( 0.000000000000000000, 0.000000000000000000, 1.000000000000000000 ) ) ;
#8448=CARTESIAN_POINT ( 'NONE',  ( 2.774999999999999911, 1.574999999999994849, -1.575000000000022160 ) ) ;
#8450=CIRCLE ( 'NONE', #5026, 2.968000000000000860 ) ;
#8453=EDGE_CURVE ( 'NONE', #11895, #5425, #157, .T. ) ;
#8454=EDGE_CURVE ( 'NONE', #10819, #2332, #3886, .T. ) ;
#8460=AXIS2_PLACEMENT_3D ( 'NONE', #1909, #8814, #593 ) ;
#8469=DIRECTION ( 'NONE',  ( 1.000000000000000000, 0.000000000000000000, 0.000000000000000000 ) ) ;
#8474=FACE_OUTER_BOUND ( 'NONE', #12176, .T. ) ;
#8484=AXIS2_PLACEMENT_3D ( 'NONE', #11287, #10298, #12573 ) ;
#8487=VERTEX_POINT ( 'NONE', #2804 ) ;
#8504=EDGE_CURVE ( 'NONE', #1907, #1198, #6401, .T. ) ;
#8505=AXIS2_PLACEMENT_3D ( 'NONE', #10476, #2594, #4970 ) ;
#8506=DIRECTION ( 'NONE',  ( -1.000000000000000000, 0.000000000000000000, 0.000000000000000000 ) ) ;
#8508=CARTESIAN_POINT ( 'NONE',  ( 0.6179999999999965521, 1.679378605318059492, 1.679378605318041506 ) ) ;
#8509=ORIENTED_EDGE ( 'NONE', *, *, #3468, .T. ) ;
#8519=CARTESIAN_POINT ( 'NONE',  ( 0.6500000000000001332, -1.679378605318047946, -1.679378605318053497 ) ) ;
#8523=AXIS2_PLACEMENT_3D ( 'NONE', #11979, #4951, #12122 ) ;
#8526=AXIS2_PLACEMENT_3D ( 'NONE', #4588, #2042, #13677 ) ;
#8528=EDGE_LOOP ( 'NONE', ( #13667, #8346 ) ) ;
#8529=DIRECTION ( 'NONE',  ( 0.000000000000000000, 0.000000000000000000, -1.000000000000000000 ) ) ;
#8533=CIRCLE ( 'NONE', #9991, 0.2944999999999998175 ) ;
#8535=AXIS2_PLACEMENT_3D ( 'NONE', #3701, #8307, #11737 ) ;
#8542=AXIS2_PLACEMENT_3D ( 'NONE', #13223, #7431, #12089 ) ;
#8544=EDGE_LOOP ( 'NONE', ( #7888, #3425, #8068, #7427 ) ) ;
#8546=LINE ( 'NONE', #13182, #8955 ) ;
#8553=DIRECTION ( 'NONE',  ( 1.000000000000000000, 0.000000000000000000, 0.000000000000000000 ) ) ;
#8559=DIRECTION ( 'NONE',  ( -1.000000000000000000, -0.000000000000000000, -0.000000000000000000 ) ) ;
#8560=FACE_OUTER_BOUND ( 'NONE', #6752, .T. ) ;
#8568=DIRECTION ( 'NONE',  ( 0.000000000000000000, 0.000000000000000000, 1.000000000000000000 ) ) ;
#8584=CYLINDRICAL_SURFACE ( 'NONE', #8542, 1.000000000000000000 ) ;
#8595=EDGE_CURVE ( 'NONE', #4331, #13435, #948, .T. ) ;
#8597=EDGE_LOOP ( 'NONE', ( #7693, #12448, #14343, #10216 ) ) ;
#8603=CARTESIAN_POINT ( 'NONE',  ( 2.156999999999998696, -1.679378605318059048, -1.416878605318056872 ) ) ;
#8608=ORIENTED_EDGE ( 'NONE', *, *, #7382, .T. ) ;
#8610=CARTESIAN_POINT ( 'NONE',  ( 0.000000000000000000, 0.000000000000000000, 0.000000000000000000 ) ) ;
#8611=EDGE_CURVE ( 'NONE', #3668, #9406, #9471, .T. ) ;
#8613=DIRECTION ( 'NONE',  ( 0.000000000000000000, 0.000000000000000000, 1.000000000000000000 ) ) ;
#8616=APPLICATION_CONTEXT ( 'automotive_design' ) ;
#8617=CARTESIAN_POINT ( 'NONE',  ( 2.774999999999999911, -1.575000000000027489, -1.574999999999989297 ) ) ;
#8627=DIRECTION ( 'NONE',  ( -1.000000000000000000, -0.000000000000000000, -0.000000000000000000 ) ) ;
#8628=DIRECTION ( 'NONE',  ( 1.000000000000000000, 0.000000000000000000, 0.000000000000000000 ) ) ;
#8629=EDGE_CURVE ( 'NONE', #1808, #3096, #13652, .T. ) ;
#8637=ORIENTED_EDGE ( 'NONE', *, *, #6140, .F. ) ;
#8638=CIRCLE ( 'NONE', #1055, 3.000000000000000444 ) ;
#8639=LINE ( 'NONE', #11932, #11628 ) ;
#8640=CARTESIAN_POINT ( 'NONE',  ( 0.000000000000000000, 1.224646799147353207E-16, -1.000000000000000000 ) ) ;
#8642=ORIENTED_EDGE ( 'NONE', *, *, #2698, .F. ) ;
#8643=CIRCLE ( 'NONE', #14487, 1.875000000000000000 ) ;
#8654=DIRECTION ( 'NONE',  ( -1.000000000000000000, 0.000000000000000000, 0.000000000000000000 ) ) ;
#8665=EDGE_CURVE ( 'NONE', #12434, #9682, #1861, .T. ) ;
#8679=CARTESIAN_POINT ( 'NONE',  ( 0.06299999999999994493, -1.679378605318048390, 1.272378605318048361 ) ) ;
#8684=AXIS2_PLACEMENT_3D ( 'NONE', #14660, #1869, #14428 ) ;
#8686=EDGE_CURVE ( 'NONE', #13039, #10392, #8005, .T. ) ;
#8688=ORIENTED_EDGE ( 'NONE', *, *, #12097, .T. ) ;
#8692=EDGE_CURVE ( 'NONE', #863, #13224, #2493, .T. ) ;
#8699=LINE ( 'NONE', #6482, #5315 ) ;
#8702=CARTESIAN_POINT ( 'NONE',  ( 2.124999999999999556, 2.360000000000015863, 1.574999999999999956 ) ) ;
#8710=EDGE_CURVE ( 'NONE', #6251, #6614, #13101, .T. ) ;
#8714=LINE ( 'NONE', #13213, #1374 ) ;
#8719=ORIENTED_EDGE ( 'NONE', *, *, #12495, .T. ) ;
#8721=CARTESIAN_POINT ( 'NONE',  ( 0.6975252985509352577, 0.000000000000000000, 0.000000000000000000 ) ) ;
#8727=EDGE_LOOP ( 'NONE', ( #13337, #1590, #9004, #7794 ) ) ;
#8732=ORIENTED_EDGE ( 'NONE', *, *, #2469, .F. ) ;
#8739=VECTOR ( 'NONE', #4267, 39.37007874015748143 ) ;
#8741=CONICAL_SURFACE ( 'NONE', #11922, 0.3750000000000007772, 0.7853981633974579379 ) ;
#8744=CARTESIAN_POINT ( 'NONE',  ( 0.09500000000000431710, -1.679378605318048390, 1.304378605318053497 ) ) ;
#8746=EDGE_CURVE ( 'NONE', #7670, #733, #3602, .T. ) ;
#8748=AXIS2_PLACEMENT_3D ( 'NONE', #15005, #6912, #12627 ) ;
#8749=CARTESIAN_POINT ( 'NONE',  ( 2.775039370078740131, -1.679378605318047946, -1.304378605318053053 ) ) ;
#8751=EDGE_LOOP ( 'NONE', ( #2459, #390, #9547, #10988, #5527, #62, #13611, #880, #8844, #12730, #8921, #14601, #3156, #14413, #5976, #1340, #1702, #3573, #2580, #14465, #5008, #13523, #10268, #3248, #3940 ) ) ;
#8763=VECTOR ( 'NONE', #11335, 39.37007874015748143 ) ;
#8766=AXIS2_PLACEMENT_3D ( 'NONE', #8357, #12070, #3965 ) ;
#8769=CONICAL_SURFACE ( 'NONE', #14872, 0.2944999999999845519, 0.7853981633974509435 ) ;
#8770=ORIENTED_EDGE ( 'NONE', *, *, #4183, .T. ) ;
#8772=AXIS2_PLACEMENT_3D ( 'NONE', #120, #2446, #10625 ) ;
#8782=CARTESIAN_POINT ( 'NONE',  ( 2.742999999999999883, -1.679378605318041950, 1.416878605318058870 ) ) ;
#8786=VECTOR ( 'NONE', #4176, 39.37007874015748143 ) ;
#8796=ORIENTED_EDGE ( 'NONE', *, *, #9557, .F. ) ;
#8802=DIRECTION ( 'NONE',  ( 1.000000000000000000, 0.000000000000000000, 0.000000000000000000 ) ) ;
#8807=DIRECTION ( 'NONE',  ( 0.7071067811865474617, 8.659560562354932858E-17, 0.7071067811865474617 ) ) ;
#8814=DIRECTION ( 'NONE',  ( -1.000000000000000000, 0.000000000000000000, 0.000000000000000000 ) ) ;
#8822=ADVANCED_FACE ( 'NONE', ( #248 ), #3943, .F. ) ;
#8827=FACE_OUTER_BOUND ( 'NONE', #7897, .T. ) ;
#8836=CARTESIAN_POINT ( 'NONE',  ( 2.774999999999999911, 1.575000000000016165, 2.359999999999999876 ) ) ;
#8840=EDGE_CURVE ( 'NONE', #3272, #8487, #15081, .T. ) ;
#8844=ORIENTED_EDGE ( 'NONE', *, *, #13612, .T. ) ;
#8848=CARTESIAN_POINT ( 'NONE',  ( 2.124999999999999556, 0.000000000000000000, 0.000000000000000000 ) ) ;
#8852=VERTEX_POINT ( 'NONE', #9759 ) ;
#8858=EDGE_CURVE ( 'NONE', #11912, #14728, #5166, .T. ) ;
#8862=ADVANCED_FACE ( 'NONE', ( #11898 ), #14479, .F. ) ;
#8866=CIRCLE ( 'NONE', #12759, 0.2944999999999998175 ) ;
#8869=ORIENTED_EDGE ( 'NONE', *, *, #6487, .F. ) ;
#8871=DIRECTION ( 'NONE',  ( 0.7071067811865467956, 0.000000000000000000, -0.7071067811865482389 ) ) ;
#8873=VERTEX_POINT ( 'NONE', #1483 ) ;
#8875=FACE_OUTER_BOUND ( 'NONE', #5311, .T. ) ;
#8877=CARTESIAN_POINT ( 'NONE',  ( 2.124999999999999556, -2.359999999999984333, 1.575000000000016387 ) ) ;
#8884=AXIS2_PLACEMENT_3D ( 'NONE', #5219, #14537, #10744 ) ;
#8893=AXIS2_PLACEMENT_3D ( 'NONE', #13942, #7842, #2007 ) ;
#8897=CARTESIAN_POINT ( 'NONE',  ( 2.124999999999999556, 0.000000000000000000, 0.000000000000000000 ) ) ;
#8900=DIRECTION ( 'NONE',  ( 0.000000000000000000, 0.000000000000000000, 1.000000000000000000 ) ) ;
#8915=ORIENTED_EDGE ( 'NONE', *, *, #13004, .F. ) ;
#8920=AXIS2_PLACEMENT_3D ( 'NONE', #13971, #2515, #14135 ) ;
#8921=ORIENTED_EDGE ( 'NONE', *, *, #9887, .T. ) ;
#8924=VECTOR ( 'NONE', #750, 39.37007874015748143 ) ;
#8929=DIRECTION ( 'NONE',  ( 0.000000000000000000, 0.000000000000000000, 1.000000000000000000 ) ) ;
#8931=DIRECTION ( 'NONE',  ( 0.7071067811865479058, 8.659560562354930393E-17, 0.7071067811865472397 ) ) ;
#8935=AXIS2_PLACEMENT_3D ( 'NONE', #8721, #10030, #14450 ) ;
#8936=CONICAL_SURFACE ( 'NONE', #8460, 0.3750000000000004996, 0.7853981633974589371 ) ;
#8944=EDGE_CURVE ( 'NONE', #11673, #8382, #5013, .T. ) ;
#8946=ORIENTED_EDGE ( 'NONE', *, *, #1785, .T. ) ;
#8947=VERTEX_POINT ( 'NONE', #13029 ) ;
#8953=DIRECTION ( 'NONE',  ( 0.000000000000000000, -1.000000000000000000, -9.182682331643740718E-16 ) ) ;
#8955=VECTOR ( 'NONE', #2719, 39.37007874015748854 ) ;
#8962=DIRECTION ( 'NONE',  ( 0.000000000000000000, 0.000000000000000000, -1.000000000000000000 ) ) ;
#8964=CARTESIAN_POINT ( 'NONE',  ( 2.743000000000000327, 1.679378605318042395, -1.941878605318058115 ) ) ;
#8965=EDGE_CURVE ( 'NONE', #14179, #13688, #6769, .T. ) ;
#8971=VERTEX_POINT ( 'NONE', #6621 ) ;
#8974=CIRCLE ( 'NONE', #7996, 0.2944999999999856066 ) ;
#8977=ADVANCED_FACE ( 'NONE', ( #5467 ), #1778, .F. ) ;
#8983=ORIENTED_EDGE ( 'NONE', *, *, #10169, .T. ) ;
#8985=CYLINDRICAL_SURFACE ( 'NONE', #5205, 0.3750000000000004996 ) ;
#8989=ORIENTED_EDGE ( 'NONE', *, *, #2103, .T. ) ;
#8998=EDGE_CURVE ( 'NONE', #969, #8382, #621, .T. ) ;
#9001=CIRCLE ( 'NONE', #4355, 1.000000000000000222 ) ;
#9002=ORIENTED_EDGE ( 'NONE', *, *, #12582, .T. ) ;
#9004=ORIENTED_EDGE ( 'NONE', *, *, #4750, .F. ) ;
#9005=VERTEX_POINT ( 'NONE', #11345 ) ;
#9016=CIRCLE ( 'NONE', #4863, 0.2624999999999994560 ) ;
#9017=CIRCLE ( 'NONE', #1175, 1.000000000000000000 ) ;
#9025=EDGE_LOOP ( 'NONE', ( #14023, #3346 ) ) ;
#9026=DIRECTION ( 'NONE',  ( -1.000000000000000000, -0.000000000000000000, -0.000000000000000000 ) ) ;
#9032=FACE_OUTER_BOUND ( 'NONE', #8597, .T. ) ;
#9040=CARTESIAN_POINT ( 'NONE',  ( 2.774999999999999911, 0.000000000000000000, 0.000000000000000000 ) ) ;
#9043=LINE ( 'NONE', #15076, #4549 ) ;
#9044=ORIENTED_EDGE ( 'NONE', *, *, #8122, .F. ) ;
#9054=CARTESIAN_POINT ( 'NONE',  ( 2.124999999999999556, 1.575000000000016387, 2.359999999999999876 ) ) ;
#9064=ORIENTED_EDGE ( 'NONE', *, *, #8965, .T. ) ;
#9065=DIRECTION ( 'NONE',  ( 0.000000000000000000, 0.000000000000000000, -1.000000000000000000 ) ) ;
#9075=DIRECTION ( 'NONE',  ( 0.000000000000000000, 0.000000000000000000, -1.000000000000000000 ) ) ;
#9076=ORIENTED_EDGE ( 'NONE', *, *, #1734, .F. ) ;
#9078=CARTESIAN_POINT ( 'NONE',  ( 2.774999999999999911, -2.360000000000016751, -1.574999999999999956 ) ) ;
#9083=ORIENTED_EDGE ( 'NONE', *, *, #13412, .F. ) ;
#9091=ORIENTED_EDGE ( 'NONE', *, *, #1243, .F. ) ;
#9093=DIRECTION ( 'NONE',  ( 0.000000000000000000, 0.000000000000000000, -1.000000000000000000 ) ) ;
#9095=VERTEX_POINT ( 'NONE', #10210 ) ;
#9099=DIRECTION ( 'NONE',  ( 0.000000000000000000, 0.000000000000000000, -1.000000000000000000 ) ) ;
#9100=ORIENTED_EDGE ( 'NONE', *, *, #1551, .F. ) ;
#9101=LINE ( 'NONE', #11389, #14781 ) ;
#9104=DIRECTION ( 'NONE',  ( 1.000000000000000000, 0.000000000000000000, 0.000000000000000000 ) ) ;
#9113=DIRECTION ( 'NONE',  ( 0.7071067811865436870, 0.000000000000000000, -0.7071067811865512365 ) ) ;
#9132=ADVANCED_FACE ( 'NONE', ( #6541 ), #2315, .F. ) ;
#9135=DIRECTION ( 'NONE',  ( 0.000000000000000000, 1.000000000000000000, -1.224646799147353207E-16 ) ) ;
#9137=EDGE_CURVE ( 'NONE', #11724, #10975, #5984, .T. ) ;
#9144=DIRECTION ( 'NONE',  ( 0.000000000000000000, 0.000000000000000000, 1.000000000000000000 ) ) ;
#9154=PLANE ( 'NONE',  #208 ) ;
#9165=CIRCLE ( 'NONE', #4287, 0.7849999999999996980 ) ;
#9175=CARTESIAN_POINT ( 'NONE',  ( 2.156999999999998696, -1.679378605318059048, -1.679378605318041950 ) ) ;
#9178=FACE_OUTER_BOUND ( 'NONE', #5474, .T. ) ;
#9185=CARTESIAN_POINT ( 'NONE',  ( 2.124999999999999556, -1.679378605318041950, 1.679378605318059048 ) ) ;
#9194=ORIENTED_EDGE ( 'NONE', *, *, #11893, .F. ) ;
#9202=AXIS2_PLACEMENT_3D ( 'NONE', #12449, #6577, #9093 ) ;
#9204=LINE ( 'NONE', #6840, #7452 ) ;
#9207=EDGE_CURVE ( 'NONE', #8150, #7356, #1319, .T. ) ;
#9209=DIRECTION ( 'NONE',  ( -1.000000000000000000, -0.000000000000000000, -0.000000000000000000 ) ) ;
#9212=ORIENTED_EDGE ( 'NONE', *, *, #2870, .F. ) ;
#9213=CARTESIAN_POINT ( 'NONE',  ( 2.774999999999999911, 3.360000000000016751, 0.9799999999999461364 ) ) ;
#9215=DIRECTION ( 'NONE',  ( 0.000000000000000000, 0.000000000000000000, 1.000000000000000000 ) ) ;
#9224=CARTESIAN_POINT ( 'NONE',  ( 2.774999999999999911, 2.359999999999999876, -1.575000000000016831 ) ) ;
#9228=ORIENTED_EDGE ( 'NONE', *, *, #13258, .T. ) ;
#9237=AXIS2_PLACEMENT_3D ( 'NONE', #5930, #8385, #13098 ) ;
#9242=ADVANCED_FACE ( 'NONE', ( #12159 ), #4133, .T. ) ;
#9247=VERTEX_POINT ( 'NONE', #5200 ) ;
#9250=AXIS2_PLACEMENT_3D ( 'NONE', #12304, #13517, #2911 ) ;
#9253=LINE ( 'NONE', #38, #11397 ) ;
#9256=EDGE_CURVE ( 'NONE', #2425, #3160, #6427, .T. ) ;
#9262=CARTESIAN_POINT ( 'NONE',  ( 2.774999999999999911, 0.000000000000000000, 0.000000000000000000 ) ) ;
#9263=AXIS2_PLACEMENT_3D ( 'NONE', #4149, #10187, #14838 ) ;
#9268=DIRECTION ( 'NONE',  ( 0.000000000000000000, 0.000000000000000000, -1.000000000000000000 ) ) ;
#9269=CARTESIAN_POINT ( 'NONE',  ( 2.774999999999999911, -1.679378605318041950, 1.679378605318059048 ) ) ;
#9275=CIRCLE ( 'NONE', #12429, 0.4070000000000058016 ) ;
#9277=FACE_BOUND ( 'NONE', #4562, .T. ) ;
#9280=EDGE_CURVE ( 'NONE', #7401, #11380, #330, .T. ) ;
#9283=VECTOR ( 'NONE', #1797, 39.37007874015748143 ) ;
#9284=ORIENTED_EDGE ( 'NONE', *, *, #12074, .T. ) ;
#9295=ORIENTED_EDGE ( 'NONE', *, *, #11949, .T. ) ;
#9304=CYLINDRICAL_SURFACE ( 'NONE', #9728, 0.3750000000000004996 ) ;
#9308=ORIENTED_EDGE ( 'NONE', *, *, #14172, .F. ) ;
#9329=EDGE_LOOP ( 'NONE', ( #536, #730, #8770, #6627 ) ) ;
#9343=DIRECTION ( 'NONE',  ( 1.000000000000000000, 0.000000000000000000, 0.000000000000000000 ) ) ;
#9353=CARTESIAN_POINT ( 'NONE',  ( 0.09500000000000431710, 1.679378605318035733, -1.679378605318065487 ) ) ;
#9360=EDGE_CURVE ( 'NONE', #193, #14590, #11357, .T. ) ;
#9363=CARTESIAN_POINT ( 'NONE',  ( 0.6500000000000001332, 1.679378605318059492, 1.272378605318037037 ) ) ;
#9364=CIRCLE ( 'NONE', #2758, 0.3750000000000007772 ) ;
#9368=DIRECTION ( 'NONE',  ( 0.000000000000000000, 0.000000000000000000, 1.000000000000000000 ) ) ;
#9369=CARTESIAN_POINT ( 'NONE',  ( 2.774999999999999911, 0.7000000000000030642, 2.399999999999999911 ) ) ;
#9376=LINE ( 'NONE', #11815, #4638 ) ;
#9377=DIRECTION ( 'NONE',  ( 1.000000000000000000, 0.000000000000000000, 0.000000000000000000 ) ) ;
#9380=EDGE_CURVE ( 'NONE', #11912, #14903, #14753, .T. ) ;
#9385=VECTOR ( 'NONE', #4451, 39.37007874015748143 ) ;
#9386=LINE ( 'NONE', #7101, #9445 ) ;
#9387=EDGE_LOOP ( 'NONE', ( #10770, #4504, #1530, #14615 ) ) ;
#9390=DIRECTION ( 'NONE',  ( 1.000000000000000000, 0.000000000000000000, 0.000000000000000000 ) ) ;
#9391=CYLINDRICAL_SURFACE ( 'NONE', #13858, 2.500000000000000444 ) ;
#9394=DIRECTION ( 'NONE',  ( -1.000000000000000000, -0.000000000000000000, -0.000000000000000000 ) ) ;
#9396=CYLINDRICAL_SURFACE ( 'NONE', #988, 0.2624999999999852451 ) ;
#9404=ORIENTED_EDGE ( 'NONE', *, *, #13318, .F. ) ;
#9406=VERTEX_POINT ( 'NONE', #1971 ) ;
#9417=EDGE_CURVE ( 'NONE', #3160, #2506, #10881, .T. ) ;
#9421=DIRECTION ( 'NONE',  ( 0.000000000000000000, 0.000000000000000000, 1.000000000000000000 ) ) ;
#9422=DIRECTION ( 'NONE',  ( 0.000000000000000000, 0.000000000000000000, -1.000000000000000000 ) ) ;
#9429=CARTESIAN_POINT ( 'NONE',  ( 2.124999999999999556, 0.9799999999999438050, -2.360000000000016307 ) ) ;
#9436=ADVANCED_FACE ( 'NONE', ( #10398 ), #1328, .F. ) ;
#9438=ORIENTED_EDGE ( 'NONE', *, *, #8216, .T. ) ;
#9439=VECTOR ( 'NONE', #229, 39.37007874015748854 ) ;
#9444=DIRECTION ( 'NONE',  ( 1.000000000000000000, 0.000000000000000000, 0.000000000000000000 ) ) ;
#9445=VECTOR ( 'NONE', #4946, 39.37007874015748143 ) ;
#9450=DIRECTION ( 'NONE',  ( 0.000000000000000000, 0.000000000000000000, 1.000000000000000000 ) ) ;
#9452=EDGE_CURVE ( 'NONE', #5573, #1719, #1086, .T. ) ;
#9453=CARTESIAN_POINT ( 'NONE',  ( 0.000000000000000000, 1.377727649040773375E-16, -1.125000000000000888 ) ) ;
#9457=CIRCLE ( 'NONE', #13325, 0.2944999999999998175 ) ;
#9459=DIRECTION ( 'NONE',  ( 1.000000000000000000, 0.000000000000000000, 0.000000000000000000 ) ) ;
#9463=EDGE_CURVE ( 'NONE', #13095, #12994, #6241, .T. ) ;
#9464=DIRECTION ( 'NONE',  ( 1.000000000000000000, 0.000000000000000000, 0.000000000000000000 ) ) ;
#9465=CARTESIAN_POINT ( 'NONE',  ( 0.6500000000000001332, 1.679378605318059492, 1.679378605318041506 ) ) ;
#9469=CARTESIAN_POINT ( 'NONE',  ( 2.156999999999999584, 1.679378605318059048, 1.679378605318041506 ) ) ;
#9470=ADVANCED_FACE ( 'NONE', ( #4357 ), #7872, .T. ) ;
#9471=CIRCLE ( 'NONE', #8484, 1.000000000000000000 ) ;
#9477=ORIENTED_EDGE ( 'NONE', *, *, #916, .T. ) ;
#9480=ORIENTED_EDGE ( 'NONE', *, *, #13547, .T. ) ;
#9487=DIRECTION ( 'NONE',  ( 0.000000000000000000, 0.000000000000000000, -1.000000000000000000 ) ) ;
#9491=EDGE_CURVE ( 'NONE', #13193, #4331, #9165, .T. ) ;
#9502=FACE_OUTER_BOUND ( 'NONE', #6116, .T. ) ;
#9506=DIRECTION ( 'NONE',  ( 0.000000000000000000, 0.000000000000000000, 1.000000000000000000 ) ) ;
#9514=CIRCLE ( 'NONE', #7786, 2.500000000000000000 ) ;
#9523=LINE ( 'NONE', #9597, #12103 ) ;
#9524=ORIENTED_EDGE ( 'NONE', *, *, #1372, .T. ) ;
#9526=LINE ( 'NONE', #8077, #5223 ) ;
#9533=CARTESIAN_POINT ( 'NONE',  ( 0.06299999999999998657, 0.000000000000000000, 0.000000000000000000 ) ) ;
#9542=FACE_OUTER_BOUND ( 'NONE', #7691, .T. ) ;
#9547=ORIENTED_EDGE ( 'NONE', *, *, #14654, .T. ) ;
#9548=CARTESIAN_POINT ( 'NONE',  ( 0.6179999999999965521, 1.679378605318059492, 1.304378605318041062 ) ) ;
#9557=EDGE_CURVE ( 'NONE', #4765, #4181, #9891, .T. ) ;
#9561=CARTESIAN_POINT ( 'NONE',  ( 0.06299999999999994493, 1.679378605318059492, 1.272378605318035927 ) ) ;
#9572=CARTESIAN_POINT ( 'NONE',  ( 2.774999999999999911, -2.359999999999984333, 1.575000000000016387 ) ) ;
#9582=CARTESIAN_POINT ( 'NONE',  ( 2.124999999999999556, -2.360000000000000320, 0.9799999999999999822 ) ) ;
#9583=DIRECTION ( 'NONE',  ( -1.000000000000000000, -0.000000000000000000, -0.000000000000000000 ) ) ;
#9588=CARTESIAN_POINT ( 'NONE',  ( 2.774999999999999911, -2.360000000000016751, -0.9799999999999431388 ) ) ;
#9591=CARTESIAN_POINT ( 'NONE',  ( 2.774999999999999911, -2.399999999999999911, 0.6999999999999997335 ) ) ;
#9593=AXIS2_PLACEMENT_3D ( 'NONE', #12626, #2147, #6839 ) ;
#9597=CARTESIAN_POINT ( 'NONE',  ( 0.06299999999999994493, 0.000000000000000000, -2.967999999999998639 ) ) ;
#9630=CARTESIAN_POINT ( 'NONE',  ( 0.7100000000000001865, 1.901497511147139923E-16, -1.552690549202460968 ) ) ;
#9643=CONICAL_SURFACE ( 'NONE', #1068, 0.3750000000000004996, 0.7853981633974621568 ) ;
#9654=CARTESIAN_POINT ( 'NONE',  ( 2.774999999999999911, -1.575000000000000178, 2.360000000000016751 ) ) ;
#9659=DIRECTION ( 'NONE',  ( 1.000000000000000000, 0.000000000000000000, 0.000000000000000000 ) ) ;
#9661=LINE ( 'NONE', #1601, #14119 ) ;
#9663=FACE_BOUND ( 'NONE', #13697, .T. ) ;
#9665=AXIS2_PLACEMENT_3D ( 'NONE', #7946, #14981, #5505 ) ;
#9670=CARTESIAN_POINT ( 'NONE',  ( 2.124999999999999556, -0.9799999999999986500, -3.359999999999999876 ) ) ;
#9678=CIRCLE ( 'NONE', #4288, 1.000000000000000222 ) ;
#9679=CONICAL_SURFACE ( 'NONE', #2328, 1.000000000000000000, 0.7853981633974477239 ) ;
#9680=DIRECTION ( 'NONE',  ( 0.000000000000000000, 0.000000000000000000, 1.000000000000000000 ) ) ;
#9682=VERTEX_POINT ( 'NONE', #410 ) ;
#9687=AXIS2_PLACEMENT_3D ( 'NONE', #427, #2529, #3970 ) ;
#9689=CYLINDRICAL_SURFACE ( 'NONE', #8523, 0.3750000000000007772 ) ;
#9693=DIRECTION ( 'NONE',  ( 1.000000000000000000, 0.000000000000000000, 0.000000000000000000 ) ) ;
#9694=ORIENTED_EDGE ( 'NONE', *, *, #7838, .F. ) ;
#9695=ORIENTED_EDGE ( 'NONE', *, *, #2452, .T. ) ;
#9698=CARTESIAN_POINT ( 'NONE',  ( 0.000000000000000000, 0.000000000000000000, 0.000000000000000000 ) ) ;
#9705=CARTESIAN_POINT ( 'NONE',  ( 2.774999999999999911, -1.575000000000027489, -2.359999999999989218 ) ) ;
#9721=ORIENTED_EDGE ( 'NONE', *, *, #10289, .T. ) ;
#9728=AXIS2_PLACEMENT_3D ( 'NONE', #3477, #5701, #4326 ) ;
#9729=CARTESIAN_POINT ( 'NONE',  ( 2.774999999999999911, -1.575000000000000178, 2.360000000000016751 ) ) ;
#9731=ORIENTED_EDGE ( 'NONE', *, *, #9207, .T. ) ;
#9732=CARTESIAN_POINT ( 'NONE',  ( 2.124999999999999556, 0.000000000000000000, 0.000000000000000000 ) ) ;
#9753=EDGE_LOOP ( 'NONE', ( #12167, #10506 ) ) ;
#9755=VERTEX_POINT ( 'NONE', #13572 ) ;
#9758=MECHANICAL_DESIGN_GEOMETRIC_PRESENTATION_REPRESENTATION('',(#15123),#12685);
#9759=CARTESIAN_POINT ( 'NONE',  ( 2.124999999999999556, -1.575000000000000178, 2.360000000000016751 ) ) ;
#9773=PRODUCT_CONTEXT ( 'NONE', #8616, 'mechanical' ) ;
#9801=LINE ( 'NONE', #3920, #2653 ) ;
#9802=ORIENTED_EDGE ( 'NONE', *, *, #8858, .T. ) ;
#9806=DIRECTION ( 'NONE',  ( -1.000000000000000000, -0.000000000000000000, -0.000000000000000000 ) ) ;
#9808=CARTESIAN_POINT ( 'NONE',  ( 0.6179999999999965521, 1.679378605318059492, 1.679378605318041506 ) ) ;
#9813=DIRECTION ( 'NONE',  ( -1.000000000000000000, -0.000000000000000000, -0.000000000000000000 ) ) ;
#9818=CARTESIAN_POINT ( 'NONE',  ( 0.06299999999999994493, 0.000000000000000000, -2.967999999999998639 ) ) ;
#9823=ORIENTED_EDGE ( 'NONE', *, *, #8038, .F. ) ;
#9835=ORIENTED_EDGE ( 'NONE', *, *, #3683, .T. ) ;
#9840=DIRECTION ( 'NONE',  ( -1.000000000000000000, -0.000000000000000000, -0.000000000000000000 ) ) ;
#9845=DIRECTION ( 'NONE',  ( -1.000000000000000000, -0.000000000000000000, -0.000000000000000000 ) ) ;
#9847=DIRECTION ( 'NONE',  ( -1.000000000000000000, -0.000000000000000000, -0.000000000000000000 ) ) ;
#9848=AXIS2_PLACEMENT_3D ( 'NONE', #8024, #2352, #109 ) ;
#9853=LINE ( 'NONE', #14507, #6325 ) ;
#9854=VECTOR ( 'NONE', #3520, 39.37007874015748143 ) ;
#9858=AXIS2_PLACEMENT_3D ( 'NONE', #3440, #6894, #11710 ) ;
#9866=VERTEX_POINT ( 'NONE', #3724 ) ;
#9870=ADVANCED_FACE ( 'NONE', ( #10603 ), #9391, .T. ) ;
#9876=CARTESIAN_POINT ( 'NONE',  ( 2.775039370078740131, 1.679378605318059492, 2.054378605318042172 ) ) ;
#9877=CARTESIAN_POINT ( 'NONE',  ( 0.6500000000000001332, -1.679378605318047946, -1.272378605318049027 ) ) ;
#9879=ORIENTED_EDGE ( 'NONE', *, *, #8965, .F. ) ;
#9883=AXIS2_PLACEMENT_3D ( 'NONE', #10645, #3321, #4838 ) ;
#9887=EDGE_CURVE ( 'NONE', #261, #13454, #4797, .T. ) ;
#9891=CIRCLE ( 'NONE', #8920, 1.124999999999998446 ) ;
#9901=EDGE_CURVE ( 'NONE', #5441, #9941, #13031, .T. ) ;
#9907=DIRECTION ( 'NONE',  ( 1.000000000000000000, 0.000000000000000000, 0.000000000000000000 ) ) ;
#9915=AXIS2_PLACEMENT_3D ( 'NONE', #3444, #6896, #9268 ) ;
#9928=LINE ( 'NONE', #489, #2422 ) ;
#9938=ORIENTED_EDGE ( 'NONE', *, *, #88, .T. ) ;
#9941=VERTEX_POINT ( 'NONE', #7250 ) ;
#9942=ORIENTED_EDGE ( 'NONE', *, *, #10825, .T. ) ;
#9951=DIRECTION ( 'NONE',  ( -1.000000000000000000, -0.000000000000000000, -0.000000000000000000 ) ) ;
#9963=DIRECTION ( 'NONE',  ( 0.000000000000000000, 0.000000000000000000, -1.000000000000000000 ) ) ;
#9965=CARTESIAN_POINT ( 'NONE',  ( 2.774999999999999911, 2.360000000000016307, 0.9799999999999454703 ) ) ;
#9972=DIRECTION ( 'NONE',  ( 1.000000000000000000, 0.000000000000000000, 0.000000000000000000 ) ) ;
#9974=AXIS2_PLACEMENT_3D ( 'NONE', #6169, #8469, #6242 ) ;
#9980=ORIENTED_EDGE ( 'NONE', *, *, #6525, .F. ) ;
#9983=ORIENTED_EDGE ( 'NONE', *, *, #2991, .F. ) ;
#9991=AXIS2_PLACEMENT_3D ( 'NONE', #9185, #12693, #8045 ) ;
#9992=PLANE ( 'NONE',  #3411 ) ;
#9994=ADVANCED_FACE ( 'NONE', ( #12047 ), #12655, .F. ) ;
#9996=EDGE_LOOP ( 'NONE', ( #13473, #4202, #11795, #844 ) ) ;
#10002=AXIS2_PLACEMENT_3D ( 'NONE', #1648, #8628, #5416 ) ;
#10006=CARTESIAN_POINT ( 'NONE',  ( 2.774999999999999911, 0.9799999999999436939, -3.360000000000016751 ) ) ;
#10009=ORIENTED_EDGE ( 'NONE', *, *, #14787, .F. ) ;
#10015=CIRCLE ( 'NONE', #14647, 0.2624999999999997335 ) ;
#10021=ORIENTED_EDGE ( 'NONE', *, *, #4977, .F. ) ;
#10022=ORIENTED_EDGE ( 'NONE', *, *, #2741, .F. ) ;
#10029=ORIENTED_EDGE ( 'NONE', *, *, #1835, .F. ) ;
#10030=DIRECTION ( 'NONE',  ( 1.000000000000000000, 0.000000000000000000, 0.000000000000000000 ) ) ;
#10031=CARTESIAN_POINT ( 'NONE',  ( 2.775039370078740131, -1.679378605318048390, 2.054378605318054607 ) ) ;
#10036=ADVANCED_FACE ( 'NONE', ( #5023 ), #9689, .F. ) ;
#10037=FACE_OUTER_BOUND ( 'NONE', #8389, .T. ) ;
#10041=CARTESIAN_POINT ( 'NONE',  ( 0.06299999999999998657, 2.296825071800860970E-16, 1.875500000000000167 ) ) ;
#10053=CIRCLE ( 'NONE', #2227, 0.4070000000000044138 ) ;
#10068=CIRCLE ( 'NONE', #13960, 0.2624999999999994560 ) ;
#10075=CARTESIAN_POINT ( 'NONE',  ( 0.6179999999999965521, -1.679378605318047946, -2.054378605318054163 ) ) ;
#10078=ORIENTED_EDGE ( 'NONE', *, *, #11565, .F. ) ;
#10081=DIRECTION ( 'NONE',  ( -0.000000000000000000, -9.182682331643740718E-16, 1.000000000000000000 ) ) ;
#10083=EDGE_CURVE ( 'NONE', #14802, #14728, #7532, .T. ) ;
#10092=ORIENTED_EDGE ( 'NONE', *, *, #10633, .T. ) ;
#10096=ORIENTED_EDGE ( 'NONE', *, *, #3796, .T. ) ;
#10098=DIRECTION ( 'NONE',  ( 0.000000000000000000, 0.000000000000000000, 1.000000000000000000 ) ) ;
#10099=DIRECTION ( 'NONE',  ( 0.000000000000000000, 0.000000000000000000, -1.000000000000000000 ) ) ;
#10102=CARTESIAN_POINT ( 'NONE',  ( 2.124999999999999556, -1.679378605318041950, 1.679378605318059048 ) ) ;
#10112=CIRCLE ( 'NONE', #1058, 1.350000000000000089 ) ;
#10127=CARTESIAN_POINT ( 'NONE',  ( 2.774999999999999911, -1.679378605318041950, 1.973878605318058810 ) ) ;
#10133=CARTESIAN_POINT ( 'NONE',  ( 2.774999999999999911, 1.679378605318042395, -1.679378605318058604 ) ) ;
#10136=CARTESIAN_POINT ( 'NONE',  ( 2.124999999999999556, 1.679378605318042395, -1.384878605318058842 ) ) ;
#10146=AXIS2_PLACEMENT_3D ( 'NONE', #11467, #6654, #10099 ) ;
#10165=EDGE_LOOP ( 'NONE', ( #9983, #4788, #14490, #14597 ) ) ;
#10168=VERTEX_POINT ( 'NONE', #6146 ) ;
#10169=EDGE_CURVE ( 'NONE', #6943, #1935, #4376, .T. ) ;
#10170=EDGE_CURVE ( 'NONE', #12552, #11912, #5105, .T. ) ;
#10173=DIRECTION ( 'NONE',  ( -1.000000000000000000, -0.000000000000000000, -0.000000000000000000 ) ) ;
#10174=EDGE_LOOP ( 'NONE', ( #3317, #10022, #3240, #5386, #77, #10021, #11841, #2609, #14495, #10915, #3835, #5175, #7848, #1620, #14251, #7982, #12852, #4384, #7495, #11738, #5464, #6398, #1701, #8086, #11652 ) ) ;
#10180=LINE ( 'NONE', #1130, #13520 ) ;
#10187=DIRECTION ( 'NONE',  ( -1.000000000000000000, -0.000000000000000000, -0.000000000000000000 ) ) ;
#10190=FACE_OUTER_BOUND ( 'NONE', #7167, .T. ) ;
#10194=CARTESIAN_POINT ( 'NONE',  ( 2.774999999999999911, -0.6999999999999990674, -2.399999999999999911 ) ) ;
#10201=DIRECTION ( 'NONE',  ( 1.000000000000000000, 0.000000000000000000, 0.000000000000000000 ) ) ;
#10205=ORIENTED_EDGE ( 'NONE', *, *, #6372, .F. ) ;
#10210=CARTESIAN_POINT ( 'NONE',  ( 2.156999999999999584, 1.679378605318059048, 1.941878605318041240 ) ) ;
#10213=CARTESIAN_POINT ( 'NONE',  ( 0.6179999999999962190, -1.679378605318048390, 1.304378605318053497 ) ) ;
#10216=ORIENTED_EDGE ( 'NONE', *, *, #12833, .T. ) ;
#10217=VECTOR ( 'NONE', #8871, 39.37007874015748143 ) ;
#10218=EDGE_CURVE ( 'NONE', #11004, #5653, #6829, .T. ) ;
#10227=FACE_BOUND ( 'NONE', #8528, .T. ) ;
#10232=CARTESIAN_POINT ( 'NONE',  ( 2.743000000000000327, 1.679378605318042395, -1.679378605318058604 ) ) ;
#10233=CIRCLE ( 'NONE', #5595, 2.500000000000000444 ) ;
#10238=EDGE_CURVE ( 'NONE', #8364, #13702, #5342, .T. ) ;
#10244=ORIENTED_EDGE ( 'NONE', *, *, #13372, .F. ) ;
#10246=FACE_OUTER_BOUND ( 'NONE', #8751, .T. ) ;
#10256=EDGE_CURVE ( 'NONE', #4101, #6363, #8042, .T. ) ;
#10263=DIRECTION ( 'NONE',  ( 1.000000000000000000, 0.000000000000000000, 0.000000000000000000 ) ) ;
#10268=ORIENTED_EDGE ( 'NONE', *, *, #2698, .T. ) ;
#10269=ADVANCED_FACE ( 'NONE', ( #13087 ), #15109, .F. ) ;
#10271=CARTESIAN_POINT ( 'NONE',  ( 2.124999999999999556, -1.679378605318059048, -1.973878605318026613 ) ) ;
#10275=ADVANCED_FACE ( 'NONE', ( #12944 ), #8769, .F. ) ;
#10277=ORIENTED_EDGE ( 'NONE', *, *, #1243, .T. ) ;
#10283=CARTESIAN_POINT ( 'NONE',  ( 2.001999999999999780, 1.726751986797767896E-16, 1.409999999999999920 ) ) ;
#10288=CARTESIAN_POINT ( 'NONE',  ( 0.6500000000000001332, 1.901497511147140416E-16, -1.552690549202460968 ) ) ;
#10289=EDGE_CURVE ( 'NONE', #4855, #5394, #1382, .T. ) ;
#10290=CARTESIAN_POINT ( 'NONE',  ( 2.774999999999999911, -2.400000000000011902, -0.6999999999999596545 ) ) ;
#10297=CIRCLE ( 'NONE', #16, 1.000000000000000666 ) ;
#10298=DIRECTION ( 'NONE',  ( -1.000000000000000000, 0.000000000000000000, 0.000000000000000000 ) ) ;
#10319=EDGE_LOOP ( 'NONE', ( #9694, #7912, #1019, #10029 ) ) ;
#10325=FACE_OUTER_BOUND ( 'NONE', #3216, .T. ) ;
#10329=PLANE ( 'NONE',  #10967 ) ;
#10342=DIRECTION ( 'NONE',  ( -1.000000000000000000, -0.000000000000000000, -0.000000000000000000 ) ) ;
#10344=CARTESIAN_POINT ( 'NONE',  ( 0.09500000000000168032, 0.000000000000000000, 0.000000000000000000 ) ) ;
#10348=VERTEX_POINT ( 'NONE', #2767 ) ;
#10359=ADVANCED_FACE ( 'NONE', ( #9663, #448 ), #1604, .F. ) ;
#10360=ADVANCED_FACE ( 'NONE', ( #7583 ), #1750, .F. ) ;
#10366=ADVANCED_FACE ( 'NONE', ( #13453 ), #14630, .F. ) ;
#10370=CARTESIAN_POINT ( 'NONE',  ( 2.774999999999999911, 1.679378605318042395, -1.416878605318059314 ) ) ;
#10372=CARTESIAN_POINT ( 'NONE',  ( 2.774999999999999911, -2.400000000000011902, -0.6999999999999596545 ) ) ;
#10377=EDGE_LOOP ( 'NONE', ( #4890, #983 ) ) ;
#10382=EDGE_CURVE ( 'NONE', #11155, #969, #372, .T. ) ;
#10384=AXIS2_PLACEMENT_3D ( 'NONE', #3357, #14828, #11242 ) ;
#10392=VERTEX_POINT ( 'NONE', #3114 ) ;
#10398=FACE_OUTER_BOUND ( 'NONE', #3358, .T. ) ;
#10405=AXIS2_PLACEMENT_3D ( 'NONE', #4136, #8802, #11244 ) ;
#10414=DIRECTION ( 'NONE',  ( -1.000000000000000000, 0.000000000000000000, 0.000000000000000000 ) ) ;
#10415=CARTESIAN_POINT ( 'NONE',  ( 0.6500000000000001332, 1.679378605318059492, 2.086378605318045754 ) ) ;
#10420=ORIENTED_EDGE ( 'NONE', *, *, #10382, .F. ) ;
#10421=CARTESIAN_POINT ( 'NONE',  ( 2.124999999999999556, -1.679378605318059048, -1.384878605318057510 ) ) ;
#10423=DIRECTION ( 'NONE',  ( -1.000000000000000000, -0.000000000000000000, -0.000000000000000000 ) ) ;
#10428=EDGE_LOOP ( 'NONE', ( #7920, #5654, #12474, #11426 ) ) ;
#10438=FACE_OUTER_BOUND ( 'NONE', #5678, .T. ) ;
#10439=FACE_OUTER_BOUND ( 'NONE', #6163, .T. ) ;
#10440=AXIS2_PLACEMENT_3D ( 'NONE', #9465, #15110, #5936 ) ;
#10441=CARTESIAN_POINT ( 'NONE',  ( 2.774999999999999911, 1.679378605318059048, 1.679378605318041506 ) ) ;
#10443=ADVANCED_FACE ( 'NONE', ( #7926 ), #2920, .F. ) ;
#10446=ORIENTED_EDGE ( 'NONE', *, *, #10169, .F. ) ;
#10465=CONICAL_SURFACE ( 'NONE', #13135, 0.2944999999999998175, 0.7853981633974536081 ) ;
#10468=CARTESIAN_POINT ( 'NONE',  ( 2.743000000000000771, 1.679378605318059048, 1.679378605318041506 ) ) ;
#10476=CARTESIAN_POINT ( 'NONE',  ( 2.001999999999999780, 0.000000000000000000, 0.000000000000000000 ) ) ;
#10482=CARTESIAN_POINT ( 'NONE',  ( 2.774999999999999911, 0.6999999999999599876, -2.400000000000011458 ) ) ;
#10484=ADVANCED_FACE ( 'NONE', ( #6941, #10227, #12437, #13873, #3416, #715 ), #9154, .F. ) ;
#10487=LINE ( 'NONE', #13829, #1652 ) ;
#10488=LINE ( 'NONE', #56, #9854 ) ;
#10495=EDGE_LOOP ( 'NONE', ( #9835, #6435, #13485, #14973 ) ) ;
#10506=ORIENTED_EDGE ( 'NONE', *, *, #5133, .T. ) ;
#10510=ORIENTED_EDGE ( 'NONE', *, *, #9137, .T. ) ;
#10512=ORIENTED_EDGE ( 'NONE', *, *, #10218, .F. ) ;
#10516=DIRECTION ( 'NONE',  ( 0.000000000000000000, -4.591341165822166182E-16, -1.000000000000000000 ) ) ;
#10518=DIRECTION ( 'NONE',  ( 1.000000000000000000, 0.000000000000000000, 0.000000000000000000 ) ) ;
#10519=DIRECTION ( 'NONE',  ( 0.000000000000000000, 0.000000000000000000, 1.000000000000000000 ) ) ;
#10525=ORIENTED_EDGE ( 'NONE', *, *, #8710, .F. ) ;
#10532=CARTESIAN_POINT ( 'NONE',  ( 0.6500000000000001332, 0.000000000000000000, 1.552690549202460968 ) ) ;
#10536=DIRECTION ( 'NONE',  ( 0.000000000000000000, 0.000000000000000000, -1.000000000000000000 ) ) ;
#10551=CARTESIAN_POINT ( 'NONE',  ( 2.774999999999999911, -1.679378605318059048, -1.384878605318056399 ) ) ;
#10554=EDGE_CURVE ( 'NONE', #5034, #2332, #9275, .T. ) ;
#10566=ORIENTED_EDGE ( 'NONE', *, *, #9463, .T. ) ;
#10567=CARTESIAN_POINT ( 'NONE',  ( 2.774999999999999911, 1.377727649040770417E-16, 1.124999999999998446 ) ) ;
#10570=CARTESIAN_POINT ( 'NONE',  ( 0.6179999999999965521, 1.679378605318035733, -1.679378605318065487 ) ) ;
#10571=CIRCLE ( 'NONE', #13003, 0.4070000000000044138 ) ;
#10572=DIRECTION ( 'NONE',  ( 0.000000000000000000, 0.000000000000000000, -1.000000000000000000 ) ) ;
#10577=CYLINDRICAL_SURFACE ( 'NONE', #4708, 0.2624999999999994560 ) ;
#10580=ORIENTED_EDGE ( 'NONE', *, *, #14787, .T. ) ;
#10593=ORIENTED_EDGE ( 'NONE', *, *, #5988, .T. ) ;
#10603=FACE_OUTER_BOUND ( 'NONE', #11342, .T. ) ;
#10607=AXIS2_PLACEMENT_3D ( 'NONE', #7491, #7416, #12150 ) ;
#10625=DIRECTION ( 'NONE',  ( 0.000000000000000000, 0.000000000000000000, -1.000000000000000000 ) ) ;
#10630=AXIS2_PLACEMENT_3D ( 'NONE', #12856, #1227, #10572 ) ;
#10633=EDGE_CURVE ( 'NONE', #5151, #13738, #4148, .T. ) ;
#10638=LINE ( 'NONE', #131, #5279 ) ;
#10640=ORIENTED_EDGE ( 'NONE', *, *, #2184, .T. ) ;
#10641=MANIFOLD_SOLID_BREP ( 'Fillet1', #304 ) ;
#10642=ORIENTED_EDGE ( 'NONE', *, *, #8454, .F. ) ;
#10645=CARTESIAN_POINT ( 'NONE',  ( 0.000000000000000000, 0.000000000000000000, 0.000000000000000000 ) ) ;
#10652=CARTESIAN_POINT ( 'NONE',  ( 2.774999999999999911, -0.6999999999999598765, 2.400000000000012346 ) ) ;
#10660=CONICAL_SURFACE ( 'NONE', #10903, 0.2944999999999998175, 0.7853981633974536081 ) ;
#10661=EDGE_LOOP ( 'NONE', ( #5924, #12339, #4655, #9404 ) ) ;
#10665=ORIENTED_EDGE ( 'NONE', *, *, #9256, .F. ) ;
#10676=ORIENTED_EDGE ( 'NONE', *, *, #12619, .F. ) ;
#10694=ORIENTED_EDGE ( 'NONE', *, *, #10289, .F. ) ;
#10695=FACE_OUTER_BOUND ( 'NONE', #4787, .T. ) ;
#10697=CYLINDRICAL_SURFACE ( 'NONE', #14335, 0.3750000000000004996 ) ;
#10701=ORIENTED_EDGE ( 'NONE', *, *, #11663, .T. ) ;
#10709=DIRECTION ( 'NONE',  ( -1.000000000000000000, -0.000000000000000000, -0.000000000000000000 ) ) ;
#10715=CIRCLE ( 'NONE', #13634, 1.552690549202460968 ) ;
#10717=CIRCLE ( 'NONE', #2888, 1.000000000000000000 ) ;
#10718=VECTOR ( 'NONE', #1053, 39.37007874015748143 ) ;
#10723=VECTOR ( 'NONE', #4879, 39.37007874015748143 ) ;
#10726=ADVANCED_FACE ( 'NONE', ( #67 ), #11224, .F. ) ;
#10727=EDGE_CURVE ( 'NONE', #4509, #2057, #6591, .T. ) ;
#10728=DIRECTION ( 'NONE',  ( 0.000000000000000000, 0.000000000000000000, 1.000000000000000000 ) ) ;
#10731=CIRCLE ( 'NONE', #4130, 2.500000000000000444 ) ;
#10736=CARTESIAN_POINT ( 'NONE',  ( 0.06299999999999994493, 1.679378605318035733, -2.086378605318071511 ) ) ;
#10742=FACE_OUTER_BOUND ( 'NONE', #13439, .T. ) ;
#10744=DIRECTION ( 'NONE',  ( 0.000000000000000000, 0.000000000000000000, -1.000000000000000000 ) ) ;
#10750=CIRCLE ( 'NONE', #1926, 0.7849999999999993650 ) ;
#10752=DIRECTION ( 'NONE',  ( 0.000000000000000000, 0.000000000000000000, 1.000000000000000000 ) ) ;
#10761=DIRECTION ( 'NONE',  ( 0.000000000000000000, 0.000000000000000000, 1.000000000000000000 ) ) ;
#10770=ORIENTED_EDGE ( 'NONE', *, *, #11963, .F. ) ;
#10782=DIRECTION ( 'NONE',  ( 1.000000000000000000, 0.000000000000000000, 0.000000000000000000 ) ) ;
#10784=CYLINDRICAL_SURFACE ( 'NONE', #7968, 0.7849999999999996980 ) ;
#10792=ORIENTED_EDGE ( 'NONE', *, *, #14654, .F. ) ;
#10799=CARTESIAN_POINT ( 'NONE',  ( 0.09500000000000431710, -1.679378605318048390, 2.054378605318054607 ) ) ;
#10801=DIRECTION ( 'NONE',  ( -0.7071067811865406894, 8.659560562355016675E-17, -0.7071067811865542341 ) ) ;
#10802=ORIENTED_EDGE ( 'NONE', *, *, #6376, .F. ) ;
#10807=VERTEX_POINT ( 'NONE', #10271 ) ;
#10813=DIRECTION ( 'NONE',  ( 0.7071067811865436870, 8.659560562354978464E-17, 0.7071067811865512365 ) ) ;
#10819=VERTEX_POINT ( 'NONE', #10799 ) ;
#10823=ADVANCED_FACE ( 'NONE', ( #7361 ), #14160, .F. ) ;
#10825=EDGE_CURVE ( 'NONE', #1772, #1104, #7291, .T. ) ;
#10827=DIRECTION ( 'NONE',  ( -1.000000000000000000, -0.000000000000000000, -0.000000000000000000 ) ) ;
#10837=EDGE_LOOP ( 'NONE', ( #13866, #7755, #8000, #5131 ) ) ;
#10838=ORIENTED_EDGE ( 'NONE', *, *, #2991, .T. ) ;
#10855=AXIS2_PLACEMENT_3D ( 'NONE', #425, #497, #2747 ) ;
#10857=FACE_OUTER_BOUND ( 'NONE', #14570, .T. ) ;
#10858=ORIENTED_EDGE ( 'NONE', *, *, #414, .T. ) ;
#10861=DIRECTION ( 'NONE',  ( 0.7071067811865436870, 8.659560562354978464E-17, 0.7071067811865512365 ) ) ;
#10866=( NAMED_UNIT ( * ) SI_UNIT ( $, .STERADIAN. ) SOLID_ANGLE_UNIT ( ) );
#10881=CIRCLE ( 'NONE', #10146, 0.2944999999999998175 ) ;
#10882=DIRECTION ( 'NONE',  ( 1.000000000000000000, 0.000000000000000000, 0.000000000000000000 ) ) ;
#10884=CIRCLE ( 'NONE', #8935, 1.494001693158433230 ) ;
#10891=DIRECTION ( 'NONE',  ( 1.000000000000000000, 0.000000000000000000, 0.000000000000000000 ) ) ;
#10893=CIRCLE ( 'NONE', #3824, 0.2625000000000000111 ) ;
#10898=ORIENTED_EDGE ( 'NONE', *, *, #8840, .T. ) ;
#10903=AXIS2_PLACEMENT_3D ( 'NONE', #1623, #6313, #2079 ) ;
#10908=ADVANCED_FACE ( 'NONE', ( #3917 ), #2155, .F. ) ;
#10912=SHAPE_REPRESENTATION ( 'Outlet Housing', ( #8424 ), #7206 ) ;
#10915=ORIENTED_EDGE ( 'NONE', *, *, #8595, .F. ) ;
#10918=ORIENTED_EDGE ( 'NONE', *, *, #8216, .F. ) ;
#10929=AXIS2_PLACEMENT_3D ( 'NONE', #8848, #2098, #4336 ) ;
#10933=CYLINDRICAL_SURFACE ( 'NONE', #10855, 0.2625000000000000111 ) ;
#10943=ORIENTED_EDGE ( 'NONE', *, *, #9137, .F. ) ;
#10948=TOROIDAL_SURFACE ( 'NONE', #169, 1.552690549202460968, 0.05999999999999999778 ) ;
#10954=DIRECTION ( 'NONE',  ( 0.000000000000000000, 0.000000000000000000, -1.000000000000000000 ) ) ;
#10959=AXIS2_PLACEMENT_3D ( 'NONE', #12602, #11545, #15062 ) ;
#10963=ADVANCED_FACE ( 'NONE', ( #8875 ), #4213, .F. ) ;
#10965=AXIS2_PLACEMENT_3D ( 'NONE', #14247, #10891, #10752 ) ;
#10967=AXIS2_PLACEMENT_3D ( 'NONE', #12763, #4675, #9422 ) ;
#10970=CIRCLE ( 'NONE', #4380, 0.2944999999999998175 ) ;
#10971=AXIS2_PLACEMENT_3D ( 'NONE', #2869, #7686, #14721 ) ;
#10975=VERTEX_POINT ( 'NONE', #5435 ) ;
#10979=CARTESIAN_POINT ( 'NONE',  ( 2.774999999999999911, 1.679378605318059048, 1.679378605318041506 ) ) ;
#10981=DIRECTION ( 'NONE',  ( 1.000000000000000000, 0.000000000000000000, 0.000000000000000000 ) ) ;
#10985=VECTOR ( 'NONE', #10813, 39.37007874015748854 ) ;
#10987=ORIENTED_EDGE ( 'NONE', *, *, #10170, .T. ) ;
#10988=ORIENTED_EDGE ( 'NONE', *, *, #9901, .T. ) ;
#11004=VERTEX_POINT ( 'NONE', #5277 ) ;
#11016=DIRECTION ( 'NONE',  ( -1.000000000000000000, -0.000000000000000000, -0.000000000000000000 ) ) ;
#11018=EDGE_CURVE ( 'NONE', #6943, #5889, #5362, .T. ) ;
#11021=EDGE_CURVE ( 'NONE', #12552, #10819, #14451, .T. ) ;
#11025=DIRECTION ( 'NONE',  ( 0.000000000000000000, 0.000000000000000000, 1.000000000000000000 ) ) ;
#11034=CIRCLE ( 'NONE', #4211, 1.812000000000000277 ) ;
#11038=ADVANCED_FACE ( 'NONE', ( #1741 ), #10465, .F. ) ;
#11045=DIRECTION ( 'NONE',  ( -0.000000000000000000, 1.000000000000000000, -0.000000000000000000 ) ) ;
#11050=EDGE_CURVE ( 'NONE', #13629, #9095, #13860, .T. ) ;
#11062=ORIENTED_EDGE ( 'NONE', *, *, #1110, .T. ) ;
#11064=CARTESIAN_POINT ( 'NONE',  ( 2.124999999999999556, -2.360000000000016751, -0.9799999999999431388 ) ) ;
#11066=AXIS2_PLACEMENT_3D ( 'NONE', #14639, #2582, #762 ) ;
#11072=EDGE_LOOP ( 'NONE', ( #673, #8203, #10512, #8312 ) ) ;
#11073=CONICAL_SURFACE ( 'NONE', #14990, 0.3750000000000004996, 0.7853981633974514986 ) ;
#11074=FACE_OUTER_BOUND ( 'NONE', #11248, .T. ) ;
#11085=CARTESIAN_POINT ( 'NONE',  ( 2.124999999999999556, 2.296212748401287479E-16, 1.875000000000000000 ) ) ;
#11086=CIRCLE ( 'NONE', #14758, 1.124999999999998446 ) ;
#11088=CARTESIAN_POINT ( 'NONE',  ( 0.06299999999999994493, -1.679378605318048390, 2.086378605318059964 ) ) ;
#11123=AXIS2_PLACEMENT_3D ( 'NONE', #5202, #13365, #14519 ) ;
#11125=EDGE_CURVE ( 'NONE', #733, #7670, #6087, .T. ) ;
#11127=VERTEX_POINT ( 'NONE', #6813 ) ;
#11129=CONICAL_SURFACE ( 'NONE', #2347, 3.000000000000000444, 0.7853981633974568277 ) ;
#11135=CYLINDRICAL_SURFACE ( 'NONE', #11899, 1.000000000000000000 ) ;
#11136=DIRECTION ( 'NONE',  ( 0.000000000000000000, -0.000000000000000000, 1.000000000000000000 ) ) ;
#11139=ORIENTED_EDGE ( 'NONE', *, *, #7230, .F. ) ;
#11143=ADVANCED_FACE ( 'NONE', ( #1127 ), #4666, .F. ) ;
#11144=CIRCLE ( 'NONE', #7731, 1.552690549202460968 ) ;
#11145=LINE ( 'NONE', #5184, #8739 ) ;
#11148=FACE_OUTER_BOUND ( 'NONE', #13356, .T. ) ;
#11155=VERTEX_POINT ( 'NONE', #4511 ) ;
#11156=ORIENTED_EDGE ( 'NONE', *, *, #2141, .F. ) ;
#11164=CARTESIAN_POINT ( 'NONE',  ( 2.001999999999999780, 0.000000000000000000, 0.000000000000000000 ) ) ;
#11176=ORIENTED_EDGE ( 'NONE', *, *, #1206, .F. ) ;
#11177=ADVANCED_FACE ( 'NONE', ( #9178 ), #13900, .T. ) ;
#11192=DIRECTION ( 'NONE',  ( 0.000000000000000000, 0.000000000000000000, -1.000000000000000000 ) ) ;
#11200=AXIS2_PLACEMENT_3D ( 'NONE', #13240, #6227, #13393 ) ;
#11202=CONICAL_SURFACE ( 'NONE', #8040, 3.000000000000000444, 0.7853981633974568277 ) ;
#11213=VECTOR ( 'NONE', #12889, 39.37007874015748143 ) ;
#11215=ORIENTED_EDGE ( 'NONE', *, *, #12563, .T. ) ;
#11224=CONICAL_SURFACE ( 'NONE', #5863, 0.3750000000000007772, 0.7853981633974536081 ) ;
#11227=CONICAL_SURFACE ( 'NONE', #12202, 1.875500000000000167, 0.7853981633974492782 ) ;
#11229=DIRECTION ( 'NONE',  ( 0.000000000000000000, 0.000000000000000000, 1.000000000000000000 ) ) ;
#11236=CARTESIAN_POINT ( 'NONE',  ( 2.156999999999998696, -1.679378605318059048, -1.679378605318041950 ) ) ;
#11242=DIRECTION ( 'NONE',  ( 0.000000000000000000, 0.000000000000000000, 1.000000000000000000 ) ) ;
#11244=DIRECTION ( 'NONE',  ( 0.000000000000000000, 0.000000000000000000, -1.000000000000000000 ) ) ;
#11248=EDGE_LOOP ( 'NONE', ( #5292, #14270, #9802, #13075 ) ) ;
#11250=LINE ( 'NONE', #11321, #289 ) ;
#11257=CARTESIAN_POINT ( 'NONE',  ( 2.124999999999999556, 1.679378605318059048, 1.679378605318041506 ) ) ;
#11263=DIRECTION ( 'NONE',  ( 1.000000000000000000, 0.000000000000000000, 0.000000000000000000 ) ) ;
#11282=EDGE_CURVE ( 'NONE', #2531, #4331, #4971, .T. ) ;
#11287=CARTESIAN_POINT ( 'NONE',  ( 0.1250000000000009992, 0.000000000000000000, 0.000000000000000000 ) ) ;
#11288=EDGE_CURVE ( 'NONE', #261, #2297, #1276, .T. ) ;
#11290=DIRECTION ( 'NONE',  ( 0.000000000000000000, 0.000000000000000000, 1.000000000000000000 ) ) ;
#11291=EDGE_CURVE ( 'NONE', #6251, #3716, #8309, .T. ) ;
#11318=VERTEX_POINT ( 'NONE', #12913 ) ;
#11321=CARTESIAN_POINT ( 'NONE',  ( 2.742999999999999883, -1.679378605318041950, 1.416878605318058870 ) ) ;
#11327=EDGE_LOOP ( 'NONE', ( #2336, #13972, #13417, #7589 ) ) ;
#11328=LINE ( 'NONE', #10194, #9385 ) ;
#11330=VECTOR ( 'NONE', #7813, 39.37007874015748143 ) ;
#11335=DIRECTION ( 'NONE',  ( 0.7071067811865516806, 0.000000000000000000, -0.7071067811865433539 ) ) ;
#11336=ORIENTED_EDGE ( 'NONE', *, *, #12794, .T. ) ;
#11339=VECTOR ( 'NONE', #5517, 39.37007874015748143 ) ;
#11341=ORIENTED_EDGE ( 'NONE', *, *, #7927, .F. ) ;
#11342=EDGE_LOOP ( 'NONE', ( #338, #1964, #12727, #8326 ) ) ;
#11345=CARTESIAN_POINT ( 'NONE',  ( 0.6179999999999965521, 1.679378605318035733, -2.054378605318066153 ) ) ;
#11346=LINE ( 'NONE', #703, #4196 ) ;
#11352=CIRCLE ( 'NONE', #14524, 2.499999999999999556 ) ;
#11353=EDGE_LOOP ( 'NONE', ( #14182, #10446, #5865, #8023 ) ) ;
#11357=CIRCLE ( 'NONE', #14040, 0.2944999999999987073 ) ;
#11375=CIRCLE ( 'NONE', #609, 1.812000000000000277 ) ;
#11380=VERTEX_POINT ( 'NONE', #5897 ) ;
#11381=VERTEX_POINT ( 'NONE', #10551 ) ;
#11389=CARTESIAN_POINT ( 'NONE',  ( 2.775039370078740131, 1.679378605318059492, 1.304378605318041062 ) ) ;
#11397=VECTOR ( 'NONE', #14202, 39.37007874015748143 ) ;
#11414=VECTOR ( 'NONE', #6812, 39.37007874015748143 ) ;
#11415=VERTEX_POINT ( 'NONE', #14433 ) ;
#11417=CARTESIAN_POINT ( 'NONE',  ( 2.124999999999999556, 1.575000000000000178, -2.360000000000016751 ) ) ;
#11418=DIRECTION ( 'NONE',  ( 1.000000000000000000, 0.000000000000000000, 0.000000000000000000 ) ) ;
#11422=EDGE_CURVE ( 'NONE', #167, #9866, #4138, .T. ) ;
#11426=ORIENTED_EDGE ( 'NONE', *, *, #1110, .F. ) ;
#11428=CONICAL_SURFACE ( 'NONE', #6311, 0.3750000000000004996, 0.7853981633974589371 ) ;
#11430=CARTESIAN_POINT ( 'NONE',  ( 2.774999999999999911, 1.575000000000016387, 2.359999999999999876 ) ) ;
#11433=EDGE_LOOP ( 'NONE', ( #14812, #9438, #4710, #2858 ) ) ;
#11436=VERTEX_POINT ( 'NONE', #8782 ) ;
#11438=ORIENTED_EDGE ( 'NONE', *, *, #12985, .F. ) ;
#11439=AXIS2_PLACEMENT_3D ( 'NONE', #5126, #13208, #1509 ) ;
#11453=AXIS2_PLACEMENT_3D ( 'NONE', #12222, #10709, #6048 ) ;
#11465=ORIENTED_EDGE ( 'NONE', *, *, #12662, .T. ) ;
#11467=CARTESIAN_POINT ( 'NONE',  ( 2.774999999999999911, -1.679378605318041950, 1.679378605318059048 ) ) ;
#11470=CARTESIAN_POINT ( 'NONE',  ( 2.774999999999999911, 2.360000000000015863, 1.574999999999999956 ) ) ;
#11474=DIRECTION ( 'NONE',  ( 0.000000000000000000, 0.000000000000000000, -1.000000000000000000 ) ) ;
#11476=FACE_OUTER_BOUND ( 'NONE', #14676, .T. ) ;
#11477=DIRECTION ( 'NONE',  ( -1.000000000000000000, -0.000000000000000000, -0.000000000000000000 ) ) ;
#11482=VECTOR ( 'NONE', #9813, 39.37007874015748143 ) ;
#11483=EDGE_CURVE ( 'NONE', #2425, #1772, #9928, .T. ) ;
#11498=ORIENTED_EDGE ( 'NONE', *, *, #12903, .F. ) ;
#11506=VERTEX_POINT ( 'NONE', #11064 ) ;
#11516=ORIENTED_EDGE ( 'NONE', *, *, #985, .T. ) ;
#11531=DIRECTION ( 'NONE',  ( -1.000000000000000000, -0.000000000000000000, -0.000000000000000000 ) ) ;
#11540=ORIENTED_EDGE ( 'NONE', *, *, #8402, .T. ) ;
#11542=DIRECTION ( 'NONE',  ( 0.000000000000000000, 0.000000000000000000, -1.000000000000000000 ) ) ;
#11545=DIRECTION ( 'NONE',  ( -1.000000000000000000, -0.000000000000000000, -0.000000000000000000 ) ) ;
#11549=DIRECTION ( 'NONE',  ( 0.000000000000000000, 0.000000000000000000, 1.000000000000000000 ) ) ;
#11550=VECTOR ( 'NONE', #14312, 39.37007874015748143 ) ;
#11558=EDGE_LOOP ( 'NONE', ( #2752, #14678, #14883, #7018 ) ) ;
#11559=ORIENTED_EDGE ( 'NONE', *, *, #11674, .F. ) ;
#11565=EDGE_CURVE ( 'NONE', #12994, #13095, #10970, .T. ) ;
#11569=AXIS2_PLACEMENT_3D ( 'NONE', #2197, #12975, #11693 ) ;
#11583=CARTESIAN_POINT ( 'NONE',  ( 2.774999999999999911, 2.360000000000000320, -0.9800000000000007594 ) ) ;
#11617=EDGE_CURVE ( 'NONE', #9682, #12994, #789, .T. ) ;
#11618=EDGE_CURVE ( 'NONE', #10168, #1992, #7805, .T. ) ;
#11620=ORIENTED_EDGE ( 'NONE', *, *, #14212, .T. ) ;
#11623=VECTOR ( 'NONE', #1535, 39.37007874015748143 ) ;
#11625=LINE ( 'NONE', #10482, #7906 ) ;
#11628=VECTOR ( 'NONE', #10861, 39.37007874015748854 ) ;
#11631=LINE ( 'NONE', #4674, #432 ) ;
#11636=DIRECTION ( 'NONE',  ( 0.000000000000000000, 0.000000000000000000, 1.000000000000000000 ) ) ;
#11645=AXIS2_PLACEMENT_3D ( 'NONE', #2510, #188, #8345 ) ;
#11652=ORIENTED_EDGE ( 'NONE', *, *, #12662, .F. ) ;
#11656=DIRECTION ( 'NONE',  ( 0.000000000000000000, 0.000000000000000000, -1.000000000000000000 ) ) ;
#11663=EDGE_CURVE ( 'NONE', #9095, #13629, #10015, .T. ) ;
#11664=DIRECTION ( 'NONE',  ( 1.000000000000000000, 0.000000000000000000, 0.000000000000000000 ) ) ;
#11665=VECTOR ( 'NONE', #4012, 39.37007874015748854 ) ;
#11672=DIRECTION ( 'NONE',  ( 1.000000000000000000, 0.000000000000000000, 0.000000000000000000 ) ) ;
#11673=VERTEX_POINT ( 'NONE', #10532 ) ;
#11674=EDGE_CURVE ( 'NONE', #9406, #3668, #2179, .T. ) ;
#11686=EDGE_CURVE ( 'NONE', #651, #10168, #8335, .T. ) ;
#11693=DIRECTION ( 'NONE',  ( 0.000000000000000000, -4.591341165821852610E-16, 1.000000000000000000 ) ) ;
#11696=FACE_OUTER_BOUND ( 'NONE', #7901, .T. ) ;
#11705=AXIS2_PLACEMENT_3D ( 'NONE', #12169, #3770, #369 ) ;
#11707=AXIS2_PLACEMENT_3D ( 'NONE', #15146, #1282, #3445 ) ;
#11710=DIRECTION ( 'NONE',  ( 0.000000000000000000, 0.000000000000000000, -1.000000000000000000 ) ) ;
#11714=CARTESIAN_POINT ( 'NONE',  ( 0.6180000000000012150, 0.000000000000000000, 0.000000000000000000 ) ) ;
#11717=CARTESIAN_POINT ( 'NONE',  ( 2.124999999999999556, -1.679378605318041950, 1.973878605318058810 ) ) ;
#11719=ORIENTED_EDGE ( 'NONE', *, *, #8692, .F. ) ;
#11724=VERTEX_POINT ( 'NONE', #9548 ) ;
#11726=CARTESIAN_POINT ( 'NONE',  ( 0.6500000000000001332, 3.654346048655703246E-16, -2.968000000000000860 ) ) ;
#11733=ORIENTED_EDGE ( 'NONE', *, *, #7310, .T. ) ;
#11737=DIRECTION ( 'NONE',  ( 0.000000000000000000, 0.000000000000000000, 1.000000000000000000 ) ) ;
#11738=ORIENTED_EDGE ( 'NONE', *, *, #1279, .F. ) ;
#11741=DIRECTION ( 'NONE',  ( 0.000000000000000000, 0.000000000000000000, 1.000000000000000000 ) ) ;
#11744=VECTOR ( 'NONE', #342, 39.37007874015748854 ) ;
#11758=DIRECTION ( 'NONE',  ( 0.000000000000000000, 0.000000000000000000, 1.000000000000000000 ) ) ;
#11766=ORIENTED_EDGE ( 'NONE', *, *, #11291, .F. ) ;
#11768=EDGE_LOOP ( 'NONE', ( #13917, #14268, #9083, #7947 ) ) ;
#11769=EDGE_CURVE ( 'NONE', #7387, #1907, #10750, .T. ) ;
#11772=ORIENTED_EDGE ( 'NONE', *, *, #10554, .T. ) ;
#11780=CIRCLE ( 'NONE', #6397, 0.2944999999999987073 ) ;
#11791=ADVANCED_FACE ( 'NONE', ( #12200 ), #9992, .F. ) ;
#11795=ORIENTED_EDGE ( 'NONE', *, *, #46, .F. ) ;
#11801=ORIENTED_EDGE ( 'NONE', *, *, #13947, .F. ) ;
#11804=CARTESIAN_POINT ( 'NONE',  ( 2.775039370078740131, -1.679378605318047946, -2.054378605318054163 ) ) ;
#11805=ORIENTED_EDGE ( 'NONE', *, *, #2870, .T. ) ;
#11811=CARTESIAN_POINT ( 'NONE',  ( 2.774999999999999911, 0.9800000000000039790, 2.359999999999999876 ) ) ;
#11815=CARTESIAN_POINT ( 'NONE',  ( 2.124999999999999556, -2.360000000000000320, 1.575000000000016387 ) ) ;
#11820=ORIENTED_EDGE ( 'NONE', *, *, #9417, .F. ) ;
#11837=ORIENTED_EDGE ( 'NONE', *, *, #171, .T. ) ;
#11840=FACE_OUTER_BOUND ( 'NONE', #15138, .T. ) ;
#11841=ORIENTED_EDGE ( 'NONE', *, *, #2797, .F. ) ;
#11847=EDGE_CURVE ( 'NONE', #5675, #4181, #7533, .T. ) ;
#11857=CARTESIAN_POINT ( 'NONE',  ( 2.774999999999999911, -1.575000000000000178, 2.360000000000016751 ) ) ;
#11859=ORIENTED_EDGE ( 'NONE', *, *, #1499, .T. ) ;
#11862=ORIENTED_EDGE ( 'NONE', *, *, #8665, .T. ) ;
#11872=CARTESIAN_POINT ( 'NONE',  ( 2.124999999999999556, -0.9799999999999990941, -2.359999999999999876 ) ) ;
#11874=ADVANCED_FACE ( 'NONE', ( #1556 ), #13164, .F. ) ;
#11875=ORIENTED_EDGE ( 'NONE', *, *, #8075, .F. ) ;
#11891=DIRECTION ( 'NONE',  ( -1.000000000000000000, -0.000000000000000000, -0.000000000000000000 ) ) ;
#11893=EDGE_CURVE ( 'NONE', #11318, #9755, #13639, .T. ) ;
#11895=VERTEX_POINT ( 'NONE', #10288 ) ;
#11898=FACE_OUTER_BOUND ( 'NONE', #13962, .T. ) ;
#11899=AXIS2_PLACEMENT_3D ( 'NONE', #9698, #9840, #4028 ) ;
#11903=DIRECTION ( 'NONE',  ( -1.000000000000000000, -0.000000000000000000, -0.000000000000000000 ) ) ;
#11905=LINE ( 'NONE', #14036, #13642 ) ;
#11912=VERTEX_POINT ( 'NONE', #10213 ) ;
#11914=VERTEX_POINT ( 'NONE', #12423 ) ;
#11922=AXIS2_PLACEMENT_3D ( 'NONE', #9353, #8506, #4836 ) ;
#11931=ORIENTED_EDGE ( 'NONE', *, *, #3432, .F. ) ;
#11932=CARTESIAN_POINT ( 'NONE',  ( 0.6179999999999965521, 1.679378605318035733, -1.304378605318064821 ) ) ;
#11934=ORIENTED_EDGE ( 'NONE', *, *, #4841, .T. ) ;
#11936=CIRCLE ( 'NONE', #11705, 0.2944999999999987073 ) ;
#11948=CARTESIAN_POINT ( 'NONE',  ( 0.6179999999999965521, -1.679378605318047946, -1.679378605318053497 ) ) ;
#11949=EDGE_CURVE ( 'NONE', #5441, #1907, #4249, .T. ) ;
#11952=CARTESIAN_POINT ( 'NONE',  ( 0.09500000000000431710, -1.679378605318047946, -1.679378605318053497 ) ) ;
#11953=LINE ( 'NONE', #518, #11550 ) ;
#11957=AXIS2_PLACEMENT_3D ( 'NONE', #8617, #12201, #1860 ) ;
#11958=DIRECTION ( 'NONE',  ( -1.000000000000000000, -0.000000000000000000, -0.000000000000000000 ) ) ;
#11962=VERTEX_POINT ( 'NONE', #2003 ) ;
#11963=EDGE_CURVE ( 'NONE', #13670, #4509, #13556, .T. ) ;
#11966=CARTESIAN_POINT ( 'NONE',  ( 0.6179999999999962190, -1.679378605318048390, 1.679378605318054163 ) ) ;
#11972=EDGE_CURVE ( 'NONE', #9005, #13668, #709, .T. ) ;
#11979=CARTESIAN_POINT ( 'NONE',  ( 2.775039370078740131, 1.679378605318035733, -1.679378605318065487 ) ) ;
#11997=CARTESIAN_POINT ( 'NONE',  ( 2.156999999999999584, 1.679378605318042395, -1.416878605318059314 ) ) ;
#12006=EDGE_LOOP ( 'NONE', ( #12498, #2268, #11062, #5644 ) ) ;
#12010=ORIENTED_EDGE ( 'NONE', *, *, #1117, .F. ) ;
#12018=FACE_OUTER_BOUND ( 'NONE', #11768, .T. ) ;
#12020=CARTESIAN_POINT ( 'NONE',  ( 2.124999999999999556, 0.9800000000000039790, 2.359999999999999876 ) ) ;
#12022=CYLINDRICAL_SURFACE ( 'NONE', #3968, 2.500000000000000000 ) ;
#12026=ORIENTED_EDGE ( 'NONE', *, *, #8692, .T. ) ;
#12031=EDGE_CURVE ( 'NONE', #2297, #4101, #9376, .T. ) ;
#12035=CIRCLE ( 'NONE', #1524, 0.2944999999999845519 ) ;
#12044=CARTESIAN_POINT ( 'NONE',  ( 2.061999999999999833, 0.000000000000000000, 0.000000000000000000 ) ) ;
#12045=CARTESIAN_POINT ( 'NONE',  ( 2.774999999999999911, -0.9799999999999986500, -3.359999999999999876 ) ) ;
#12047=FACE_OUTER_BOUND ( 'NONE', #1887, .T. ) ;
#12052=ADVANCED_FACE ( 'NONE', ( #85 ), #11227, .T. ) ;
#12054=AXIS2_PLACEMENT_3D ( 'NONE', #9269, #7050, #9421 ) ;
#12070=DIRECTION ( 'NONE',  ( -1.000000000000000000, 0.000000000000000000, 0.000000000000000000 ) ) ;
#12071=CIRCLE ( 'NONE', #10607, 1.812500000000000222 ) ;
#12074=EDGE_CURVE ( 'NONE', #12552, #14802, #237, .T. ) ;
#12075=ORIENTED_EDGE ( 'NONE', *, *, #6468, .F. ) ;
#12078=ORIENTED_EDGE ( 'NONE', *, *, #13935, .F. ) ;
#12089=DIRECTION ( 'NONE',  ( 0.000000000000000000, 0.000000000000000000, 1.000000000000000000 ) ) ;
#12097=EDGE_CURVE ( 'NONE', #13668, #13702, #382, .T. ) ;
#12101=EDGE_LOOP ( 'NONE', ( #2705, #883, #1383, #8408 ) ) ;
#12103=VECTOR ( 'NONE', #2704, 39.37007874015748854 ) ;
#12122=DIRECTION ( 'NONE',  ( 0.000000000000000000, 0.000000000000000000, 1.000000000000000000 ) ) ;
#12141=ORIENTED_EDGE ( 'NONE', *, *, #10238, .T. ) ;
#12150=DIRECTION ( 'NONE',  ( 0.000000000000000000, 0.000000000000000000, 1.000000000000000000 ) ) ;
#12159=FACE_OUTER_BOUND ( 'NONE', #2331, .T. ) ;
#12162=CARTESIAN_POINT ( 'NONE',  ( 2.774999999999999911, 2.360000000000015863, 1.574999999999999956 ) ) ;
#12167=ORIENTED_EDGE ( 'NONE', *, *, #14457, .T. ) ;
#12169=CARTESIAN_POINT ( 'NONE',  ( 2.774999999999999911, 1.679378605318059048, 1.679378605318041506 ) ) ;
#12173=CIRCLE ( 'NONE', #12652, 1.000000000000000444 ) ;
#12175=CARTESIAN_POINT ( 'NONE',  ( 0.6179999999999965521, -1.679378605318047946, -1.679378605318053497 ) ) ;
#12176=EDGE_LOOP ( 'NONE', ( #14302, #10205, #3502, #8732 ) ) ;
#12177=AXIS2_PLACEMENT_3D ( 'NONE', #13154, #4840, #7145 ) ;
#12181=CIRCLE ( 'NONE', #5841, 1.000000000000000666 ) ;
#12183=AXIS2_PLACEMENT_3D ( 'NONE', #11952, #8654, #13373 ) ;
#12193=VERTEX_POINT ( 'NONE', #6448 ) ;
#12197=DIRECTION ( 'NONE',  ( 0.000000000000000000, 0.000000000000000000, 1.000000000000000000 ) ) ;
#12200=FACE_OUTER_BOUND ( 'NONE', #6886, .T. ) ;
#12201=DIRECTION ( 'NONE',  ( 1.000000000000000000, 0.000000000000000000, 0.000000000000000000 ) ) ;
#12202=AXIS2_PLACEMENT_3D ( 'NONE', #9533, #10518, #2558 ) ;
#12222=CARTESIAN_POINT ( 'NONE',  ( 2.774999999999999911, -1.679378605318041950, 1.679378605318059048 ) ) ;
#12224=ORIENTED_EDGE ( 'NONE', *, *, #7466, .F. ) ;
#12239=EDGE_LOOP ( 'NONE', ( #8161, #10510, #7825, #112 ) ) ;
#12241=DIRECTION ( 'NONE',  ( -1.000000000000000000, -0.000000000000000000, -0.000000000000000000 ) ) ;
#12245=CARTESIAN_POINT ( 'NONE',  ( 0.6180000000000012150, 0.000000000000000000, 0.000000000000000000 ) ) ;
#12255=LINE ( 'NONE', #13178, #8197 ) ;
#12258=ORIENTED_EDGE ( 'NONE', *, *, #11483, .T. ) ;
#12264=ORIENTED_EDGE ( 'NONE', *, *, #11018, .F. ) ;
#12279=CARTESIAN_POINT ( 'NONE',  ( 2.124999999999999556, 0.7000000000000030642, 2.399999999999999911 ) ) ;
#12280=FACE_OUTER_BOUND ( 'NONE', #13945, .T. ) ;
#12303=DIRECTION ( 'NONE',  ( 0.7071067811865460184, 8.659560562354951347E-17, 0.7071067811865490160 ) ) ;
#12304=CARTESIAN_POINT ( 'NONE',  ( 2.156999999999999584, 1.679378605318059048, 1.679378605318041506 ) ) ;
#12307=APPLICATION_CONTEXT ( 'automotive_design' ) ;
#12309=VECTOR ( 'NONE', #8123, 39.37007874015748143 ) ;
#12312=EDGE_LOOP ( 'NONE', ( #14714, #5869 ) ) ;
#12318=CARTESIAN_POINT ( 'NONE',  ( 2.774999999999999911, 0.9800000000000039790, 3.360000000000000320 ) ) ;
#12323=ORIENTED_EDGE ( 'NONE', *, *, #7005, .F. ) ;
#12335=CARTESIAN_POINT ( 'NONE',  ( 0.06299999999999994493, 1.679378605318035733, -1.272378605318059686 ) ) ;
#12337=EDGE_LOOP ( 'NONE', ( #11156, #11875, #8719, #7438 ) ) ;
#12339=ORIENTED_EDGE ( 'NONE', *, *, #6553, .T. ) ;
#12351=CIRCLE ( 'NONE', #13807, 2.499999999999999556 ) ;
#12354=ORIENTED_EDGE ( 'NONE', *, *, #12813, .F. ) ;
#12355=CARTESIAN_POINT ( 'NONE',  ( 2.124999999999999556, -1.575000000000016387, -2.359999999999999876 ) ) ;
#12362=CONICAL_SURFACE ( 'NONE', #14814, 0.2624999999999997335, 0.7853981633974479459 ) ;
#12363=DIRECTION ( 'NONE',  ( 0.000000000000000000, 0.000000000000000000, -1.000000000000000000 ) ) ;
#12372=AXIS2_PLACEMENT_3D ( 'NONE', #9630, #406, #13264 ) ;
#12410=CARTESIAN_POINT ( 'NONE',  ( 2.775039370078740131, -1.679378605318047946, -1.679378605318053497 ) ) ;
#12413=DIRECTION ( 'NONE',  ( 1.000000000000000000, 0.000000000000000000, 0.000000000000000000 ) ) ;
#12414=ORIENTED_EDGE ( 'NONE', *, *, #7230, .T. ) ;
#12418=DIRECTION ( 'NONE',  ( -1.000000000000000000, -0.000000000000000000, -0.000000000000000000 ) ) ;
#12423=CARTESIAN_POINT ( 'NONE',  ( 2.124999999999999556, 1.679378605318059048, 1.384878605318041744 ) ) ;
#12429=AXIS2_PLACEMENT_3D ( 'NONE', #1610, #9390, #8529 ) ;
#12434=VERTEX_POINT ( 'NONE', #11997 ) ;
#12437=FACE_BOUND ( 'NONE', #5107, .T. ) ;
#12447=ORIENTED_EDGE ( 'NONE', *, *, #7095, .T. ) ;
#12448=ORIENTED_EDGE ( 'NONE', *, *, #11282, .F. ) ;
#12449=CARTESIAN_POINT ( 'NONE',  ( 0.09500000000000431710, 1.679378605318035733, -1.679378605318065487 ) ) ;
#12450=ORIENTED_EDGE ( 'NONE', *, *, #3468, .F. ) ;
#12456=ORIENTED_EDGE ( 'NONE', *, *, #7011, .F. ) ;
#12464=DIRECTION ( 'NONE',  ( 0.7071067811865496822, 0.000000000000000000, -0.7071067811865452413 ) ) ;
#12466=DIRECTION ( 'NONE',  ( 0.000000000000000000, 0.000000000000000000, 1.000000000000000000 ) ) ;
#12469=ORIENTED_EDGE ( 'NONE', *, *, #14979, .T. ) ;
#12473=CARTESIAN_POINT ( 'NONE',  ( 2.774999999999999911, -2.360000000000016751, -0.9799999999999431388 ) ) ;
#12474=ORIENTED_EDGE ( 'NONE', *, *, #15000, .F. ) ;
#12479=ORIENTED_EDGE ( 'NONE', *, *, #5208, .F. ) ;
#12480=ORIENTED_EDGE ( 'NONE', *, *, #6452, .F. ) ;
#12495=EDGE_CURVE ( 'NONE', #13702, #7063, #2742, .T. ) ;
#12498=ORIENTED_EDGE ( 'NONE', *, *, #5767, .F. ) ;
#12515=ORIENTED_EDGE ( 'NONE', *, *, #414, .F. ) ;
#12521=DIRECTION ( 'NONE',  ( 1.000000000000000000, 0.000000000000000000, 0.000000000000000000 ) ) ;
#12522=ORIENTED_EDGE ( 'NONE', *, *, #2469, .T. ) ;
#12531=EDGE_CURVE ( 'NONE', #5110, #3609, #5109, .T. ) ;
#12533=VECTOR ( 'NONE', #14234, 39.37007874015748143 ) ;
#12545=CARTESIAN_POINT ( 'NONE',  ( 2.774999999999999911, -0.9799999999999986500, -3.359999999999999876 ) ) ;
#12552=VERTEX_POINT ( 'NONE', #1878 ) ;
#12558=DIRECTION ( 'NONE',  ( -0.9781476007338071321, 0.000000000000000000, 0.2079116908177521816 ) ) ;
#12563=EDGE_CURVE ( 'NONE', #1935, #2080, #14738, .T. ) ;
#12565=AXIS2_PLACEMENT_3D ( 'NONE', #5986, #1596, #4058 ) ;
#12569=PRODUCT_DEFINITION_CONTEXT ( 'detailed design', #12307, 'design' ) ;
#12573=DIRECTION ( 'NONE',  ( 0.000000000000000000, 0.000000000000000000, -1.000000000000000000 ) ) ;
#12575=DIRECTION ( 'NONE',  ( -1.000000000000000000, 0.000000000000000000, 0.000000000000000000 ) ) ;
#12579=DIRECTION ( 'NONE',  ( 1.000000000000000000, 0.000000000000000000, 0.000000000000000000 ) ) ;
#12582=EDGE_CURVE ( 'NONE', #10975, #7670, #11145, .T. ) ;
#12585=CIRCLE ( 'NONE', #1595, 0.2944999999999856066 ) ;
#12586=CIRCLE ( 'NONE', #4551, 0.05999999999999990757 ) ;
#12601=CARTESIAN_POINT ( 'NONE',  ( 2.124999999999999556, -1.575000000000000178, 2.360000000000016751 ) ) ;
#12602=CARTESIAN_POINT ( 'NONE',  ( 0.6500000000000001332, 1.679378605318059492, 1.679378605318041506 ) ) ;
#12603=DIRECTION ( 'NONE',  ( -1.000000000000000000, -0.000000000000000000, -0.000000000000000000 ) ) ;
#12607=CARTESIAN_POINT ( 'NONE',  ( 2.650000000000001688, 0.000000000000000000, -1.000000000000000000 ) ) ;
#12608=CIRCLE ( 'NONE', #3830, 0.2624999999999852451 ) ;
#12618=ORIENTED_EDGE ( 'NONE', *, *, #13935, .T. ) ;
#12619=EDGE_CURVE ( 'NONE', #1160, #1793, #14381, .T. ) ;
#12621=ORIENTED_EDGE ( 'NONE', *, *, #14722, .F. ) ;
#12626=CARTESIAN_POINT ( 'NONE',  ( 2.124999999999999556, -1.679378605318059048, -1.679378605318041950 ) ) ;
#12627=DIRECTION ( 'NONE',  ( 0.000000000000000000, 0.000000000000000000, -1.000000000000000000 ) ) ;
#12633=ORIENTED_EDGE ( 'NONE', *, *, #12985, .T. ) ;
#12652=AXIS2_PLACEMENT_3D ( 'NONE', #7132, #55, #13908 ) ;
#12655=TOROIDAL_SURFACE ( 'NONE', #9974, 1.409999999999999920, 0.05999999999999999778 ) ;
#12662=EDGE_CURVE ( 'NONE', #14785, #7387, #6343, .T. ) ;
#12684=EDGE_CURVE ( 'NONE', #1691, #2057, #7625, .T. ) ;
#12685=( GEOMETRIC_REPRESENTATION_CONTEXT ( 3 ) GLOBAL_UNCERTAINTY_ASSIGNED_CONTEXT ( ( #4333 ) ) GLOBAL_UNIT_ASSIGNED_CONTEXT ( ( #14625, #4158, #3079 ) ) REPRESENTATION_CONTEXT ( 'NONE', 'WORKASPACE' ) );
#12686=DIRECTION ( 'NONE',  ( -1.000000000000000000, -0.000000000000000000, -0.000000000000000000 ) ) ;
#12692=FACE_OUTER_BOUND ( 'NONE', #2040, .T. ) ;
#12693=DIRECTION ( 'NONE',  ( 1.000000000000000000, 0.000000000000000000, 0.000000000000000000 ) ) ;
#12700=ORIENTED_EDGE ( 'NONE', *, *, #7538, .F. ) ;
#12716=DIRECTION ( 'NONE',  ( -0.7071067811865447972, 8.659560562354964906E-17, -0.7071067811865501263 ) ) ;
#12722=CIRCLE ( 'NONE', #5407, 0.2625000000000000111 ) ;
#12726=ORIENTED_EDGE ( 'NONE', *, *, #2773, .F. ) ;
#12727=ORIENTED_EDGE ( 'NONE', *, *, #1279, .T. ) ;
#12730=ORIENTED_EDGE ( 'NONE', *, *, #3723, .T. ) ;
#12739=CARTESIAN_POINT ( 'NONE',  ( 2.774999999999999911, 1.575000000000016387, 2.359999999999999876 ) ) ;
#12751=ORIENTED_EDGE ( 'NONE', *, *, #11686, .F. ) ;
#12758=DIRECTION ( 'NONE',  ( 0.000000000000000000, 0.000000000000000000, -1.000000000000000000 ) ) ;
#12759=AXIS2_PLACEMENT_3D ( 'NONE', #1284, #8359, #5825 ) ;
#12760=FACE_OUTER_BOUND ( 'NONE', #13486, .T. ) ;
#12763=CARTESIAN_POINT ( 'NONE',  ( 2.061999999999999389, 1.812000000000000277, 0.000000000000000000 ) ) ;
#12771=CARTESIAN_POINT ( 'NONE',  ( 0.000000000000000000, 0.000000000000000000, 0.000000000000000000 ) ) ;
#12777=AXIS2_PLACEMENT_3D ( 'NONE', #1836, #3158, #14847 ) ;
#12779=CONICAL_SURFACE ( 'NONE', #6209, 1.350000000000000089, 0.2094395102393122321 ) ;
#12783=CARTESIAN_POINT ( 'NONE',  ( 0.6179999999999962190, -1.679378605318048390, 1.679378605318054163 ) ) ;
#12785=DIRECTION ( 'NONE',  ( 0.000000000000000000, 0.000000000000000000, -1.000000000000000000 ) ) ;
#12789=ORIENTED_EDGE ( 'NONE', *, *, #9360, .F. ) ;
#12794=EDGE_CURVE ( 'NONE', #651, #4021, #6022, .T. ) ;
#12795=CARTESIAN_POINT ( 'NONE',  ( 2.743000000000000771, 1.679378605318059048, 1.679378605318041506 ) ) ;
#12800=ORIENTED_EDGE ( 'NONE', *, *, #10170, .F. ) ;
#12813=EDGE_CURVE ( 'NONE', #7174, #14092, #7328, .T. ) ;
#12815=FACE_OUTER_BOUND ( 'NONE', #10661, .T. ) ;
#12816=DIRECTION ( 'NONE',  ( 0.000000000000000000, 0.000000000000000000, -1.000000000000000000 ) ) ;
#12823=CIRCLE ( 'NONE', #4784, 0.3750000000000004996 ) ;
#12830=ORIENTED_EDGE ( 'NONE', *, *, #5708, .F. ) ;
#12833=EDGE_CURVE ( 'NONE', #3096, #13193, #11905, .T. ) ;
#12837=VECTOR ( 'NONE', #3330, 39.37007874015748143 ) ;
#12852=ORIENTED_EDGE ( 'NONE', *, *, #2184, .F. ) ;
#12856=CARTESIAN_POINT ( 'NONE',  ( 2.743000000000000327, 1.679378605318042395, -1.679378605318058604 ) ) ;
#12865=ORIENTED_EDGE ( 'NONE', *, *, #11021, .F. ) ;
#12866=VECTOR ( 'NONE', #2734, 39.37007874015748143 ) ;
#12877=DIRECTION ( 'NONE',  ( 0.000000000000000000, 0.000000000000000000, -1.000000000000000000 ) ) ;
#12882=PLANE ( 'NONE',  #4302 ) ;
#12888=EDGE_LOOP ( 'NONE', ( #12479, #8983, #14725, #10701 ) ) ;
#12889=DIRECTION ( 'NONE',  ( -0.000000000000000000, 1.000000000000000000, -0.000000000000000000 ) ) ;
#12890=AXIS2_PLACEMENT_3D ( 'NONE', #3556, #9377, #7010 ) ;
#12893=VECTOR ( 'NONE', #7780, 39.37007874015748143 ) ;
#12894=AXIS2_PLACEMENT_3D ( 'NONE', #6899, #8046, #1133 ) ;
#12902=AXIS2_PLACEMENT_3D ( 'NONE', #9654, #14379, #3695 ) ;
#12903=EDGE_CURVE ( 'NONE', #13224, #2178, #5851, .T. ) ;
#12904=ORIENTED_EDGE ( 'NONE', *, *, #1372, .F. ) ;
#12912=FACE_OUTER_BOUND ( 'NONE', #4922, .T. ) ;
#12913=CARTESIAN_POINT ( 'NONE',  ( 2.774999999999999911, 2.360000000000000320, -0.9800000000000007594 ) ) ;
#12915=AXIS2_PLACEMENT_3D ( 'NONE', #5968, #15068, #126 ) ;
#12920=VECTOR ( 'NONE', #10081, 39.37007874015748143 ) ;
#12921=DIRECTION ( 'NONE',  ( 0.000000000000000000, 0.000000000000000000, -1.000000000000000000 ) ) ;
#12931=EDGE_LOOP ( 'NONE', ( #11438, #1659, #12010, #13790 ) ) ;
#12933=CARTESIAN_POINT ( 'NONE',  ( 0.09500000000000431710, -1.679378605318047946, -1.679378605318053497 ) ) ;
#12940=VECTOR ( 'NONE', #13856, 39.37007874015748143 ) ;
#12944=FACE_OUTER_BOUND ( 'NONE', #679, .T. ) ;
#12951=ORIENTED_EDGE ( 'NONE', *, *, #10218, .T. ) ;
#12955=EDGE_CURVE ( 'NONE', #3096, #2531, #440, .T. ) ;
#12958=EDGE_LOOP ( 'NONE', ( #6788, #9731 ) ) ;
#12959=EDGE_LOOP ( 'NONE', ( #3483, #14369, #12141, #14474 ) ) ;
#12968=CARTESIAN_POINT ( 'NONE',  ( 2.774999999999999911, 1.575000000000000178, -2.360000000000016751 ) ) ;
#12971=ADVANCED_FACE ( 'NONE', ( #8155 ), #13940, .F. ) ;
#12973=VECTOR ( 'NONE', #12716, 39.37007874015748854 ) ;
#12975=DIRECTION ( 'NONE',  ( -0.000000000000000000, 1.000000000000000000, 4.591341165821852610E-16 ) ) ;
#12982=VERTEX_POINT ( 'NONE', #14797 ) ;
#12985=EDGE_CURVE ( 'NONE', #2425, #11436, #13125, .T. ) ;
#12991=DIRECTION ( 'NONE',  ( -1.000000000000000000, -0.000000000000000000, -0.000000000000000000 ) ) ;
#12992=FACE_BOUND ( 'NONE', #13122, .T. ) ;
#12994=VERTEX_POINT ( 'NONE', #13782 ) ;
#13003=AXIS2_PLACEMENT_3D ( 'NONE', #8519, #5286, #294 ) ;
#13004=EDGE_CURVE ( 'NONE', #11380, #14026, #7994, .T. ) ;
#13006=DIRECTION ( 'NONE',  ( -1.000000000000000000, -0.000000000000000000, -0.000000000000000000 ) ) ;
#13007=CARTESIAN_POINT ( 'NONE',  ( 2.774999999999999911, 0.000000000000000000, 0.000000000000000000 ) ) ;
#13012=ORIENTED_EDGE ( 'NONE', *, *, #1734, .T. ) ;
#13015=CARTESIAN_POINT ( 'NONE',  ( 2.124999999999999556, 1.679378605318042395, -1.679378605318058604 ) ) ;
#13021=ADVANCED_FACE ( 'NONE', ( #10438 ), #9304, .F. ) ;
#13029=CARTESIAN_POINT ( 'NONE',  ( 2.742999999999998995, -1.679378605318059048, -1.416878605318056872 ) ) ;
#13031=LINE ( 'NONE', #6942, #10723 ) ;
#13039=VERTEX_POINT ( 'NONE', #10290 ) ;
#13050=ORIENTED_EDGE ( 'NONE', *, *, #11963, .T. ) ;
#13056=EDGE_CURVE ( 'NONE', #11912, #12552, #1398, .T. ) ;
#13061=DIRECTION ( 'NONE',  ( 1.000000000000000000, 0.000000000000000000, 0.000000000000000000 ) ) ;
#13062=EDGE_CURVE ( 'NONE', #1193, #7063, #1886, .T. ) ;
#13070=ORIENTED_EDGE ( 'NONE', *, *, #3906, .T. ) ;
#13072=AXIS2_PLACEMENT_3D ( 'NONE', #8448, #11958, #2626 ) ;
#13073=DIRECTION ( 'NONE',  ( 0.000000000000000000, 0.000000000000000000, -1.000000000000000000 ) ) ;
#13075=ORIENTED_EDGE ( 'NONE', *, *, #10083, .F. ) ;
#13084=CARTESIAN_POINT ( 'NONE',  ( 2.124999999999999556, 2.399999999999999911, -0.7000000000000009548 ) ) ;
#13087=FACE_OUTER_BOUND ( 'NONE', #12006, .T. ) ;
#13092=ORIENTED_EDGE ( 'NONE', *, *, #8122, .T. ) ;
#13095=VERTEX_POINT ( 'NONE', #2406 ) ;
#13098=DIRECTION ( 'NONE',  ( 0.000000000000000000, 0.000000000000000000, 1.000000000000000000 ) ) ;
#13101=CIRCLE ( 'NONE', #3841, 0.05999999999999990757 ) ;
#13109=AXIS2_PLACEMENT_3D ( 'NONE', #13198, #2735, #407 ) ;
#13116=AXIS2_PLACEMENT_3D ( 'NONE', #4435, #6963, #13676 ) ;
#13122=EDGE_LOOP ( 'NONE', ( #15133, #9695 ) ) ;
#13125=CIRCLE ( 'NONE', #5087, 0.2625000000000000111 ) ;
#13129=CARTESIAN_POINT ( 'NONE',  ( 0.6180000000000012150, 0.000000000000000000, 0.000000000000000000 ) ) ;
#13133=VECTOR ( 'NONE', #13954, 39.37007874015748143 ) ;
#13134=DIRECTION ( 'NONE',  ( -1.000000000000000000, -0.000000000000000000, -0.000000000000000000 ) ) ;
#13135=AXIS2_PLACEMENT_3D ( 'NONE', #10102, #7646, #14686 ) ;
#13140=ADVANCED_FACE ( 'NONE', ( #1318 ), #5574, .F. ) ;
#13141=ORIENTED_EDGE ( 'NONE', *, *, #8944, .F. ) ;
#13149=CONICAL_SURFACE ( 'NONE', #12915, 1.350000000000000089, 0.2094395102393122321 ) ;
#13153=VECTOR ( 'NONE', #151, 39.37007874015748143 ) ;
#13154=CARTESIAN_POINT ( 'NONE',  ( 0.09500000000000431710, 1.679378605318035733, -1.679378605318065487 ) ) ;
#13159=AXIS2_PLACEMENT_3D ( 'NONE', #380, #14466, #5453 ) ;
#13164=CONICAL_SURFACE ( 'NONE', #1190, 1.000000000000000000, 0.7853981633974477239 ) ;
#13165=DIRECTION ( 'NONE',  ( -1.000000000000000000, -0.000000000000000000, -0.000000000000000000 ) ) ;
#13171=AXIS2_PLACEMENT_3D ( 'NONE', #1146, #8062, #4688 ) ;
#13176=DIRECTION ( 'NONE',  ( -0.7071067811865400232, 0.000000000000000000, 0.7071067811865551223 ) ) ;
#13177=ADVANCED_FACE ( 'NONE', ( #3782 ), #8026, .F. ) ;
#13178=CARTESIAN_POINT ( 'NONE',  ( 0.000000000000000000, 1.653273178848927113E-16, -1.350000000000000089 ) ) ;
#13182=CARTESIAN_POINT ( 'NONE',  ( 0.6180000000000012150, 3.673940397442060361E-16, -3.000000000000000444 ) ) ;
#13193=VERTEX_POINT ( 'NONE', #13310 ) ;
#13198=CARTESIAN_POINT ( 'NONE',  ( 0.06299999999999998657, 0.000000000000000000, 0.000000000000000000 ) ) ;
#13208=DIRECTION ( 'NONE',  ( -1.000000000000000000, -0.000000000000000000, 0.000000000000000000 ) ) ;
#13213=CARTESIAN_POINT ( 'NONE',  ( 2.774999999999999911, -0.9799999999999990941, -2.359999999999999876 ) ) ;
#13215=ORIENTED_EDGE ( 'NONE', *, *, #9207, .F. ) ;
#13218=EDGE_LOOP ( 'NONE', ( #13675, #7610, #3336, #13141 ) ) ;
#13223=CARTESIAN_POINT ( 'NONE',  ( 2.774999999999999911, -3.360000000000016751, -0.9799999999999434719 ) ) ;
#13224=VERTEX_POINT ( 'NONE', #605 ) ;
#13226=DIRECTION ( 'NONE',  ( -1.000000000000000000, -0.000000000000000000, -0.000000000000000000 ) ) ;
#13235=VECTOR ( 'NONE', #12241, 39.37007874015748143 ) ;
#13240=CARTESIAN_POINT ( 'NONE',  ( 0.06299999999999998657, 0.000000000000000000, 0.000000000000000000 ) ) ;
#13242=DIRECTION ( 'NONE',  ( -1.000000000000000000, -0.000000000000000000, -0.000000000000000000 ) ) ;
#13247=ORIENTED_EDGE ( 'NONE', *, *, #3442, .F. ) ;
#13257=CONICAL_SURFACE ( 'NONE', #9858, 0.2624999999999994560, 0.7853981633974446153 ) ;
#13258=EDGE_CURVE ( 'NONE', #11127, #1772, #6799, .T. ) ;
#13262=EDGE_LOOP ( 'NONE', ( #1705, #6866 ) ) ;
#13264=DIRECTION ( 'NONE',  ( 0.000000000000000000, -1.224646799147354933E-16, 1.000000000000000000 ) ) ;
#13275=CARTESIAN_POINT ( 'NONE',  ( 0.06299999999999994493, -1.679378605318047946, -1.679378605318053497 ) ) ;
#13286=EDGE_LOOP ( 'NONE', ( #12951, #573 ) ) ;
#13287=ORIENTED_EDGE ( 'NONE', *, *, #13947, .T. ) ;
#13291=ORIENTED_EDGE ( 'NONE', *, *, #4997, .T. ) ;
#13293=DIRECTION ( 'NONE',  ( 0.7071067811865479058, 0.000000000000000000, -0.7071067811865472397 ) ) ;
#13295=AXIS2_PLACEMENT_3D ( 'NONE', #6558, #1791, #11136 ) ;
#13297=CARTESIAN_POINT ( 'NONE',  ( 2.124999999999999556, 2.296212748401287479E-16, 1.875000000000000000 ) ) ;
#13306=DIRECTION ( 'NONE',  ( 0.000000000000000000, 0.000000000000000000, 1.000000000000000000 ) ) ;
#13310=CARTESIAN_POINT ( 'NONE',  ( 2.124999999999999556, -2.360000000000016751, -1.574999999999999956 ) ) ;
#13311=CARTESIAN_POINT ( 'NONE',  ( 2.124999999999999556, 3.360000000000016751, 0.9799999999999461364 ) ) ;
#13318=EDGE_CURVE ( 'NONE', #8947, #1719, #5757, .T. ) ;
#13323=ADVANCED_FACE ( 'NONE', ( #14854 ), #2574, .T. ) ;
#13325=AXIS2_PLACEMENT_3D ( 'NONE', #13704, #6767, #2163 ) ;
#13326=LINE ( 'NONE', #10136, #7383 ) ;
#13334=AXIS2_PLACEMENT_3D ( 'NONE', #10006, #5481, #8006 ) ;
#13335=EDGE_LOOP ( 'NONE', ( #3507, #4498, #91, #10642 ) ) ;
#13337=ORIENTED_EDGE ( 'NONE', *, *, #2797, .T. ) ;
#13338=DIRECTION ( 'NONE',  ( 0.7071067811865516806, 8.659560562354882322E-17, 0.7071067811865433539 ) ) ;
#13347=TOROIDAL_SURFACE ( 'NONE', #8505, 1.409999999999999920, 0.05999999999999999778 ) ;
#13348=EDGE_CURVE ( 'NONE', #11127, #11415, #9204, .T. ) ;
#13356=EDGE_LOOP ( 'NONE', ( #13946, #4501, #878, #1889 ) ) ;
#13365=DIRECTION ( 'NONE',  ( -1.000000000000000000, 0.000000000000000000, 0.000000000000000000 ) ) ;
#13372=EDGE_CURVE ( 'NONE', #2396, #167, #830, .T. ) ;
#13373=DIRECTION ( 'NONE',  ( 0.000000000000000000, 0.000000000000000000, -1.000000000000000000 ) ) ;
#13376=DIRECTION ( 'NONE',  ( 1.000000000000000000, 0.000000000000000000, 0.000000000000000000 ) ) ;
#13378=CIRCLE ( 'NONE', #8766, 0.3750000000000004996 ) ;
#13380=DIRECTION ( 'NONE',  ( -1.000000000000000000, -0.000000000000000000, -0.000000000000000000 ) ) ;
#13382=ORIENTED_EDGE ( 'NONE', *, *, #13602, .T. ) ;
#13385=VERTEX_POINT ( 'NONE', #14932 ) ;
#13393=DIRECTION ( 'NONE',  ( 0.000000000000000000, 0.000000000000000000, 1.000000000000000000 ) ) ;
#13396=DIRECTION ( 'NONE',  ( -1.000000000000000000, -0.000000000000000000, 0.000000000000000000 ) ) ;
#13405=ORIENTED_EDGE ( 'NONE', *, *, #5878, .T. ) ;
#13412=EDGE_CURVE ( 'NONE', #13039, #1808, #6970, .T. ) ;
#13417=ORIENTED_EDGE ( 'NONE', *, *, #2964, .F. ) ;
#13426=CYLINDRICAL_SURFACE ( 'NONE', #5322, 1.000000000000000222 ) ;
#13435=VERTEX_POINT ( 'NONE', #11872 ) ;
#13439=EDGE_LOOP ( 'NONE', ( #14475, #12354, #14047, #5399 ) ) ;
#13451=CARTESIAN_POINT ( 'NONE',  ( 0.09500000000000431710, -1.679378605318048390, 1.679378605318054163 ) ) ;
#13453=FACE_OUTER_BOUND ( 'NONE', #186, .T. ) ;
#13454=VERTEX_POINT ( 'NONE', #3766 ) ;
#13463=EDGE_CURVE ( 'NONE', #9247, #4088, #8450, .T. ) ;
#13471=ORIENTED_EDGE ( 'NONE', *, *, #8075, .T. ) ;
#13473=ORIENTED_EDGE ( 'NONE', *, *, #198, .T. ) ;
#13485=ORIENTED_EDGE ( 'NONE', *, *, #13612, .F. ) ;
#13486=EDGE_LOOP ( 'NONE', ( #9212, #8369, #12258, #2226 ) ) ;
#13494=FACE_OUTER_BOUND ( 'NONE', #10165, .T. ) ;
#13509=EDGE_CURVE ( 'NONE', #1808, #11506, #5915, .T. ) ;
#13513=DIRECTION ( 'NONE',  ( 0.7071067811865496822, 8.659560562354905741E-17, 0.7071067811865452413 ) ) ;
#13517=DIRECTION ( 'NONE',  ( -1.000000000000000000, -0.000000000000000000, -0.000000000000000000 ) ) ;
#13520=VECTOR ( 'NONE', #14912, 39.37007874015748143 ) ;
#13523=ORIENTED_EDGE ( 'NONE', *, *, #11618, .T. ) ;
#13535=VECTOR ( 'NONE', #13006, 39.37007874015748143 ) ;
#13540=DIRECTION ( 'NONE',  ( -1.000000000000000000, -0.000000000000000000, -0.000000000000000000 ) ) ;
#13547=EDGE_CURVE ( 'NONE', #5886, #10348, #14773, .T. ) ;
#13556=LINE ( 'NONE', #1085, #12940 ) ;
#13572=CARTESIAN_POINT ( 'NONE',  ( 2.124999999999999556, 2.360000000000000320, -0.9800000000000007594 ) ) ;
#13574=CARTESIAN_POINT ( 'NONE',  ( 2.774999999999999911, 0.7000000000000030642, 2.399999999999999911 ) ) ;
#13581=ADVANCED_FACE ( 'NONE', ( #2466 ), #1297, .F. ) ;
#13586=VERTEX_POINT ( 'NONE', #7503 ) ;
#13590=PLANE ( 'NONE',  #2401 ) ;
#13596=AXIS2_PLACEMENT_3D ( 'NONE', #1554, #2791, #7246 ) ;
#13602=EDGE_CURVE ( 'NONE', #12982, #2178, #1744, .T. ) ;
#13605=CIRCLE ( 'NONE', #401, 0.9999999999999998890 ) ;
#13610=DIRECTION ( 'NONE',  ( -1.000000000000000000, 0.000000000000000000, -0.000000000000000000 ) ) ;
#13611=ORIENTED_EDGE ( 'NONE', *, *, #2110, .T. ) ;
#13612=EDGE_CURVE ( 'NONE', #7174, #8323, #7648, .T. ) ;
#13613=FACE_OUTER_BOUND ( 'NONE', #11072, .T. ) ;
#13621=CARTESIAN_POINT ( 'NONE',  ( 2.774999999999999911, -1.679378605318059048, -1.416878605318056872 ) ) ;
#13629=VERTEX_POINT ( 'NONE', #3214 ) ;
#13634=AXIS2_PLACEMENT_3D ( 'NONE', #14856, #13540, #14631 ) ;
#13638=AXIS2_PLACEMENT_3D ( 'NONE', #7223, #3466, #4 ) ;
#13639=LINE ( 'NONE', #11583, #13884 ) ;
#13641=EDGE_CURVE ( 'NONE', #5162, #4450, #11352, .T. ) ;
#13642=VECTOR ( 'NONE', #3799, 39.37007874015748143 ) ;
#13652=LINE ( 'NONE', #9078, #7274 ) ;
#13667=ORIENTED_EDGE ( 'NONE', *, *, #15000, .T. ) ;
#13668=VERTEX_POINT ( 'NONE', #2129 ) ;
#13670=VERTEX_POINT ( 'NONE', #814 ) ;
#13673=CARTESIAN_POINT ( 'NONE',  ( 2.124999999999999556, -1.575000000000027489, -2.359999999999989218 ) ) ;
#13675=ORIENTED_EDGE ( 'NONE', *, *, #1856, .F. ) ;
#13676=DIRECTION ( 'NONE',  ( 0.000000000000000000, 0.000000000000000000, 1.000000000000000000 ) ) ;
#13677=DIRECTION ( 'NONE',  ( 0.000000000000000000, 0.000000000000000000, 1.000000000000000000 ) ) ;
#13683=CARTESIAN_POINT ( 'NONE',  ( 1.375000000000000000, 0.000000000000000000, 1.350000000000000089 ) ) ;
#13684=LINE ( 'NONE', #5373, #11339 ) ;
#13685=FACE_OUTER_BOUND ( 'NONE', #11327, .T. ) ;
#13688=VERTEX_POINT ( 'NONE', #6821 ) ;
#13697=EDGE_LOOP ( 'NONE', ( #6481, #10898 ) ) ;
#13702=VERTEX_POINT ( 'NONE', #4187 ) ;
#13704=CARTESIAN_POINT ( 'NONE',  ( 2.124999999999999556, 1.679378605318059048, 1.679378605318041506 ) ) ;
#13706=CARTESIAN_POINT ( 'NONE',  ( 0.000000000000000000, 3.673940397442060361E-16, -3.000000000000000444 ) ) ;
#13713=ADVANCED_FACE ( 'NONE', ( #12280 ), #6336, .F. ) ;
#13717=ORIENTED_EDGE ( 'NONE', *, *, #4183, .F. ) ;
#13720=EDGE_LOOP ( 'NONE', ( #11540, #12522 ) ) ;
#13730=ADVANCED_FACE ( 'NONE', ( #5250 ), #8214, .F. ) ;
#13738=VERTEX_POINT ( 'NONE', #5179 ) ;
#13742=DIRECTION ( 'NONE',  ( -1.000000000000000000, -0.000000000000000000, -0.000000000000000000 ) ) ;
#13743=ORIENTED_EDGE ( 'NONE', *, *, #2880, .F. ) ;
#13748=DIRECTION ( 'NONE',  ( 1.000000000000000000, 0.000000000000000000, 0.000000000000000000 ) ) ;
#13751=CONICAL_SURFACE ( 'NONE', #8893, 2.967999999999998639, 0.7853981633974482790 ) ;
#13753=LINE ( 'NONE', #8964, #11330 ) ;
#13760=ORIENTED_EDGE ( 'NONE', *, *, #1876, .F. ) ;
#13765=DIRECTION ( 'NONE',  ( 0.000000000000000000, 0.000000000000000000, -1.000000000000000000 ) ) ;
#13772=PRODUCT_DEFINITION ( 'UNKNOWN', '', #817, #12569 ) ;
#13777=ORIENTED_EDGE ( 'NONE', *, *, #5294, .T. ) ;
#13782=CARTESIAN_POINT ( 'NONE',  ( 2.124999999999999556, 1.679378605318042395, -1.973878605318058588 ) ) ;
#13783=AXIS2_PLACEMENT_3D ( 'NONE', #5158, #13396, #9680 ) ;
#13785=CARTESIAN_POINT ( 'NONE',  ( 2.156999999999999140, -1.679378605318041950, 1.679378605318059048 ) ) ;
#13786=ADVANCED_FACE ( 'NONE', ( #10190 ), #8936, .F. ) ;
#13790=ORIENTED_EDGE ( 'NONE', *, *, #1007, .F. ) ;
#13799=DIRECTION ( 'NONE',  ( 1.000000000000000000, 0.000000000000000000, 0.000000000000000000 ) ) ;
#13800=EDGE_CURVE ( 'NONE', #8150, #937, #6441, .T. ) ;
#13807=AXIS2_PLACEMENT_3D ( 'NONE', #8386, #2251, #5931 ) ;
#13811=DIRECTION ( 'NONE',  ( 0.000000000000000000, 0.000000000000000000, 1.000000000000000000 ) ) ;
#13814=DIRECTION ( 'NONE',  ( -1.000000000000000000, -0.000000000000000000, -0.000000000000000000 ) ) ;
#13816=ORIENTED_EDGE ( 'NONE', *, *, #5124, .T. ) ;
#13817=FACE_BOUND ( 'NONE', #13720, .T. ) ;
#13819=DIRECTION ( 'NONE',  ( 1.000000000000000000, 0.000000000000000000, 0.000000000000000000 ) ) ;
#13820=EDGE_LOOP ( 'NONE', ( #5905, #14510 ) ) ;
#13823=ADVANCED_FACE ( 'NONE', ( #13685 ), #7815, .F. ) ;
#13829=CARTESIAN_POINT ( 'NONE',  ( 2.124999999999999556, -1.679378605318059048, -1.973878605318026613 ) ) ;
#13833=CONICAL_SURFACE ( 'NONE', #13109, 1.875500000000000167, 0.7853981633974492782 ) ;
#13835=ORIENTED_EDGE ( 'NONE', *, *, #8944, .T. ) ;
#13844=DIRECTION ( 'NONE',  ( -0.7071067811865436870, 8.659560562354978464E-17, -0.7071067811865512365 ) ) ;
#13856=DIRECTION ( 'NONE',  ( -0.7071067811865422437, 8.659560562354996953E-17, -0.7071067811865527908 ) ) ;
#13858=AXIS2_PLACEMENT_3D ( 'NONE', #5873, #5940, #7022 ) ;
#13860=CIRCLE ( 'NONE', #9250, 0.2624999999999997335 ) ;
#13861=DIRECTION ( 'NONE',  ( 0.000000000000000000, 4.591341165822166182E-16, 1.000000000000000000 ) ) ;
#13866=ORIENTED_EDGE ( 'NONE', *, *, #2741, .T. ) ;
#13869=VECTOR ( 'NONE', #9806, 39.37007874015748143 ) ;
#13873=FACE_BOUND ( 'NONE', #5055, .T. ) ;
#13884=VECTOR ( 'NONE', #2170, 39.37007874015748143 ) ;
#13898=ORIENTED_EDGE ( 'NONE', *, *, #13463, .F. ) ;
#13900=CYLINDRICAL_SURFACE ( 'NONE', #1898, 2.500000000000000444 ) ;
#13908=DIRECTION ( 'NONE',  ( 0.000000000000000000, 0.000000000000000000, 1.000000000000000000 ) ) ;
#13911=LINE ( 'NONE', #6974, #12309 ) ;
#13915=FACE_BOUND ( 'NONE', #984, .T. ) ;
#13917=ORIENTED_EDGE ( 'NONE', *, *, #3855, .T. ) ;
#13931=AXIS2_PLACEMENT_3D ( 'NONE', #7560, #14587, #11229 ) ;
#13932=FACE_OUTER_BOUND ( 'NONE', #8184, .T. ) ;
#13935=EDGE_CURVE ( 'NONE', #1992, #2828, #13990, .T. ) ;
#13936=CARTESIAN_POINT ( 'NONE',  ( 2.774999999999999911, 1.575000000000016609, 1.575000000000000178 ) ) ;
#13940=CYLINDRICAL_SURFACE ( 'NONE', #8279, 1.000000000000000444 ) ;
#13942=CARTESIAN_POINT ( 'NONE',  ( 0.06299999999999994493, 0.000000000000000000, 0.000000000000000000 ) ) ;
#13945=EDGE_LOOP ( 'NONE', ( #3453, #1547, #7651, #7453 ) ) ;
#13946=ORIENTED_EDGE ( 'NONE', *, *, #6553, .F. ) ;
#13947=EDGE_CURVE ( 'NONE', #12193, #4855, #12823, .T. ) ;
#13951=CARTESIAN_POINT ( 'NONE',  ( 2.001999999999999780, 0.000000000000000000, -1.409999999999999920 ) ) ;
#13954=DIRECTION ( 'NONE',  ( 0.000000000000000000, 0.000000000000000000, -1.000000000000000000 ) ) ;
#13960=AXIS2_PLACEMENT_3D ( 'NONE', #10232, #6566, #955 ) ;
#13962=EDGE_LOOP ( 'NONE', ( #3109, #9823, #14593, #1330 ) ) ;
#13963=FACE_OUTER_BOUND ( 'NONE', #4053, .T. ) ;
#13966=DIRECTION ( 'NONE',  ( 1.000000000000000000, 0.000000000000000000, 0.000000000000000000 ) ) ;
#13967=ORIENTED_EDGE ( 'NONE', *, *, #6525, .T. ) ;
#13971=CARTESIAN_POINT ( 'NONE',  ( 2.774999999999999911, 0.000000000000000000, 0.000000000000000000 ) ) ;
#13972=ORIENTED_EDGE ( 'NONE', *, *, #3989, .F. ) ;
#13973=CARTESIAN_POINT ( 'NONE',  ( 0.09500000000000431710, 1.679378605318059492, 1.679378605318041506 ) ) ;
#13981=DIRECTION ( 'NONE',  ( 0.000000000000000000, 0.000000000000000000, 1.000000000000000000 ) ) ;
#13988=ADVANCED_FACE ( 'NONE', ( #1138 ), #9679, .F. ) ;
#13990=LINE ( 'NONE', #3523, #840 ) ;
#13991=DIRECTION ( 'NONE',  ( 0.000000000000000000, 0.000000000000000000, -1.000000000000000000 ) ) ;
#14001=CARTESIAN_POINT ( 'NONE',  ( 0.6500000000000001332, 1.679378605318035733, -1.679378605318065487 ) ) ;
#14006=DIRECTION ( 'NONE',  ( 0.000000000000000000, 0.000000000000000000, 1.000000000000000000 ) ) ;
#14008=LINE ( 'NONE', #8379, #9439 ) ;
#14016=DIRECTION ( 'NONE',  ( 0.000000000000000000, 0.000000000000000000, -1.000000000000000000 ) ) ;
#14023=ORIENTED_EDGE ( 'NONE', *, *, #14263, .T. ) ;
#14026=VERTEX_POINT ( 'NONE', #15074 ) ;
#14027=CARTESIAN_POINT ( 'NONE',  ( 2.124999999999999556, 0.000000000000000000, -1.875000000000000000 ) ) ;
#14036=CARTESIAN_POINT ( 'NONE',  ( 2.774999999999999911, -2.360000000000016751, -1.574999999999999956 ) ) ;
#14037=CARTESIAN_POINT ( 'NONE',  ( 0.6975252985509352577, 1.829624391447200865E-16, -1.494001693158432786 ) ) ;
#14040=AXIS2_PLACEMENT_3D ( 'NONE', #6730, #13742, #9099 ) ;
#14047=ORIENTED_EDGE ( 'NONE', *, *, #3562, .F. ) ;
#14051=ORIENTED_EDGE ( 'NONE', *, *, #1300, .T. ) ;
#14052=CARTESIAN_POINT ( 'NONE',  ( 2.061999999999999389, 1.726751986797767896E-16, 1.409999999999999920 ) ) ;
#14060=DIRECTION ( 'NONE',  ( -1.000000000000000000, -0.000000000000000000, -0.000000000000000000 ) ) ;
#14061=DIRECTION ( 'NONE',  ( 0.000000000000000000, 0.000000000000000000, 1.000000000000000000 ) ) ;
#14067=CYLINDRICAL_SURFACE ( 'NONE', #3819, 1.000000000000000000 ) ;
#14073=DIRECTION ( 'NONE',  ( -1.000000000000000000, -0.000000000000000000, -0.000000000000000000 ) ) ;
#14092=VERTEX_POINT ( 'NONE', #2749 ) ;
#14099=EDGE_CURVE ( 'NONE', #13668, #5653, #8639, .T. ) ;
#14102=ORIENTED_EDGE ( 'NONE', *, *, #1801, .T. ) ;
#14119=VECTOR ( 'NONE', #6293, 39.37007874015748143 ) ;
#14126=EDGE_LOOP ( 'NONE', ( #3315, #1310, #10244, #266 ) ) ;
#14129=CARTESIAN_POINT ( 'NONE',  ( 0.6179999999999965521, 1.679378605318059492, 1.679378605318041506 ) ) ;
#14132=FACE_OUTER_BOUND ( 'NONE', #8004, .T. ) ;
#14135=DIRECTION ( 'NONE',  ( 0.000000000000000000, 0.000000000000000000, -1.000000000000000000 ) ) ;
#14141=AXIS2_PLACEMENT_3D ( 'NONE', #3623, #9444, #1306 ) ;
#14154=ORIENTED_EDGE ( 'NONE', *, *, #13547, .F. ) ;
#14156=EDGE_CURVE ( 'NONE', #1198, #4697, #1845, .T. ) ;
#14160=PLANE ( 'NONE',  #12902 ) ;
#14168=DIRECTION ( 'NONE',  ( -1.000000000000000000, -0.000000000000000000, -0.000000000000000000 ) ) ;
#14170=CARTESIAN_POINT ( 'NONE',  ( 2.124999999999999556, 2.360000000000015863, 1.574999999999999956 ) ) ;
#14172=EDGE_CURVE ( 'NONE', #14996, #3585, #10638, .T. ) ;
#14179=VERTEX_POINT ( 'NONE', #4831 ) ;
#14182=ORIENTED_EDGE ( 'NONE', *, *, #12563, .F. ) ;
#14189=ORIENTED_EDGE ( 'NONE', *, *, #14705, .T. ) ;
#14202=DIRECTION ( 'NONE',  ( -1.000000000000000000, -0.000000000000000000, -0.000000000000000000 ) ) ;
#14203=EDGE_LOOP ( 'NONE', ( #1428, #8025, #12323, #8227 ) ) ;
#14209=EDGE_CURVE ( 'NONE', #5886, #12434, #2095, .T. ) ;
#14212=EDGE_CURVE ( 'NONE', #10807, #6236, #7009, .T. ) ;
#14227=ORIENTED_EDGE ( 'NONE', *, *, #1551, .T. ) ;
#14234=DIRECTION ( 'NONE',  ( -1.000000000000000000, -0.000000000000000000, -0.000000000000000000 ) ) ;
#14240=ORIENTED_EDGE ( 'NONE', *, *, #8746, .F. ) ;
#14243=CIRCLE ( 'NONE', #11066, 1.875500000000000167 ) ;
#14244=CARTESIAN_POINT ( 'NONE',  ( 0.6179999999999962190, -1.679378605318048390, 2.054378605318054607 ) ) ;
#14247=CARTESIAN_POINT ( 'NONE',  ( 0.6975252985509352577, 0.000000000000000000, 0.000000000000000000 ) ) ;
#14251=ORIENTED_EDGE ( 'NONE', *, *, #10256, .F. ) ;
#14253=ORIENTED_EDGE ( 'NONE', *, *, #11972, .F. ) ;
#14263=EDGE_CURVE ( 'NONE', #14728, #14802, #7248, .T. ) ;
#14267=DIRECTION ( 'NONE',  ( 0.000000000000000000, 0.000000000000000000, -1.000000000000000000 ) ) ;
#14268=ORIENTED_EDGE ( 'NONE', *, *, #13509, .F. ) ;
#14270=ORIENTED_EDGE ( 'NONE', *, *, #13056, .F. ) ;
#14272=VECTOR ( 'NONE', #12418, 39.37007874015748143 ) ;
#14274=CARTESIAN_POINT ( 'NONE',  ( 0.09500000000000431710, -1.679378605318048390, 2.054378605318054607 ) ) ;
#14280=ORIENTED_EDGE ( 'NONE', *, *, #11422, .F. ) ;
#14300=( CONVERSION_BASED_UNIT ( 'INCH', #6206 ) LENGTH_UNIT ( ) NAMED_UNIT ( #6287 ) );
#14302=ORIENTED_EDGE ( 'NONE', *, *, #8407, .F. ) ;
#14306=EDGE_CURVE ( 'NONE', #1972, #1062, #9386, .T. ) ;
#14312=DIRECTION ( 'NONE',  ( -1.000000000000000000, -0.000000000000000000, -0.000000000000000000 ) ) ;
#14313=AXIS2_PLACEMENT_3D ( 'NONE', #5778, #9459, #12877 ) ;
#14314=DIRECTION ( 'NONE',  ( -1.000000000000000000, -0.000000000000000000, -0.000000000000000000 ) ) ;
#14316=ORIENTED_EDGE ( 'NONE', *, *, #14457, .F. ) ;
#14323=ADVANCED_FACE ( 'NONE', ( #92, #15107, #4874, #4791, #9542, #3647 ), #12882, .F. ) ;
#14335=AXIS2_PLACEMENT_3D ( 'NONE', #1425, #5892, #3671 ) ;
#14336=CARTESIAN_POINT ( 'NONE',  ( 1.375000000000000000, 0.000000000000000000, 0.000000000000000000 ) ) ;
#14338=DIRECTION ( 'NONE',  ( 0.000000000000000000, 0.000000000000000000, 1.000000000000000000 ) ) ;
#14339=AXIS2_PLACEMENT_3D ( 'NONE', #8610, #5235, #1706 ) ;
#14343=ORIENTED_EDGE ( 'NONE', *, *, #12955, .F. ) ;
#14355=DIRECTION ( 'NONE',  ( -1.000000000000000000, -0.000000000000000000, -0.000000000000000000 ) ) ;
#14366=EDGE_LOOP ( 'NONE', ( #9879, #868, #10096, #14227 ) ) ;
#14369=ORIENTED_EDGE ( 'NONE', *, *, #805, .T. ) ;
#14378=AXIS2_PLACEMENT_3D ( 'NONE', #12783, #7076, #14006 ) ;
#14379=DIRECTION ( 'NONE',  ( 0.000000000000000000, 0.000000000000000000, -1.000000000000000000 ) ) ;
#14380=VECTOR ( 'NONE', #5964, 39.37007874015748143 ) ;
#14381=CIRCLE ( 'NONE', #7546, 2.967999999999998639 ) ;
#14384=DIRECTION ( 'NONE',  ( -0.000000000000000000, -1.000000000000000000, -0.000000000000000000 ) ) ;
#14387=EDGE_CURVE ( 'NONE', #11436, #2425, #10893, .T. ) ;
#14389=AXIS2_PLACEMENT_3D ( 'NONE', #1022, #12575, #11290 ) ;
#14407=DIRECTION ( 'NONE',  ( -1.000000000000000000, -0.000000000000000000, -0.000000000000000000 ) ) ;
#14410=FACE_OUTER_BOUND ( 'NONE', #13335, .T. ) ;
#14413=ORIENTED_EDGE ( 'NONE', *, *, #13412, .T. ) ;
#14415=DIRECTION ( 'NONE',  ( -0.7071067811865414665, 0.000000000000000000, 0.7071067811865534569 ) ) ;
#14428=DIRECTION ( 'NONE',  ( 0.000000000000000000, 0.000000000000000000, -1.000000000000000000 ) ) ;
#14429=SHAPE_DEFINITION_REPRESENTATION ( #7626, #10912 ) ;
#14432=CARTESIAN_POINT ( 'NONE',  ( 2.124999999999999556, -3.360000000000016751, -0.9799999999999434719 ) ) ;
#14433=CARTESIAN_POINT ( 'NONE',  ( 2.124999999999999556, -1.679378605318041950, 1.384878605318059064 ) ) ;
#14436=CARTESIAN_POINT ( 'NONE',  ( 2.774999999999999911, -1.575000000000027489, -2.359999999999989218 ) ) ;
#14437=CARTESIAN_POINT ( 'NONE',  ( 2.124999999999999556, 1.679378605318059048, 1.679378605318041506 ) ) ;
#14450=DIRECTION ( 'NONE',  ( 0.000000000000000000, 0.000000000000000000, 1.000000000000000000 ) ) ;
#14451=LINE ( 'NONE', #10031, #3143 ) ;
#14453=EDGE_CURVE ( 'NONE', #9247, #6889, #2643, .T. ) ;
#14454=CARTESIAN_POINT ( 'NONE',  ( 2.124999999999999556, -1.574999999999984190, 1.575000000000033040 ) ) ;
#14455=EDGE_CURVE ( 'NONE', #4088, #14179, #8546, .T. ) ;
#14456=ORIENTED_EDGE ( 'NONE', *, *, #6452, .T. ) ;
#14457=EDGE_CURVE ( 'NONE', #863, #12982, #11375, .T. ) ;
#14458=DIRECTION ( 'NONE',  ( 1.000000000000000000, 0.000000000000000000, 0.000000000000000000 ) ) ;
#14461=DIRECTION ( 'NONE',  ( 0.000000000000000000, 0.000000000000000000, 1.000000000000000000 ) ) ;
#14465=ORIENTED_EDGE ( 'NONE', *, *, #4750, .T. ) ;
#14466=DIRECTION ( 'NONE',  ( 1.000000000000000000, 0.000000000000000000, 0.000000000000000000 ) ) ;
#14474=ORIENTED_EDGE ( 'NONE', *, *, #12097, .F. ) ;
#14475=ORIENTED_EDGE ( 'NONE', *, *, #4381, .T. ) ;
#14478=AXIS2_PLACEMENT_3D ( 'NONE', #185, #8102, #13811 ) ;
#14479=PLANE ( 'NONE',  #13596 ) ;
#14480=ADVANCED_FACE ( 'NONE', ( #7458 ), #10660, .F. ) ;
#14483=DIRECTION ( 'NONE',  ( 0.000000000000000000, 0.000000000000000000, -1.000000000000000000 ) ) ;
#14487=AXIS2_PLACEMENT_3D ( 'NONE', #3549, #7001, #9215 ) ;
#14489=EDGE_LOOP ( 'NONE', ( #5220, #5242, #5153, #6803 ) ) ;
#14490=ORIENTED_EDGE ( 'NONE', *, *, #10382, .T. ) ;
#14492=FACE_OUTER_BOUND ( 'NONE', #1445, .T. ) ;
#14495=ORIENTED_EDGE ( 'NONE', *, *, #14833, .F. ) ;
#14497=DIRECTION ( 'NONE',  ( 0.000000000000000000, 0.000000000000000000, -1.000000000000000000 ) ) ;
#14499=CIRCLE ( 'NONE', #15004, 1.000000000000000222 ) ;
#14500=ADVANCED_FACE ( 'NONE', ( #3013 ), #845, .F. ) ;
#14501=EDGE_CURVE ( 'NONE', #3716, #11155, #12586, .T. ) ;
#14507=CARTESIAN_POINT ( 'NONE',  ( 2.124999999999999556, 1.679378605318059048, 1.973878605318041268 ) ) ;
#14510=ORIENTED_EDGE ( 'NONE', *, *, #831, .T. ) ;
#14519=DIRECTION ( 'NONE',  ( 0.000000000000000000, 0.000000000000000000, -1.000000000000000000 ) ) ;
#14524=AXIS2_PLACEMENT_3D ( 'NONE', #4365, #14757, #14835 ) ;
#14537=DIRECTION ( 'NONE',  ( -1.000000000000000000, 0.000000000000000000, 0.000000000000000000 ) ) ;
#14540=LENGTH_MEASURE_WITH_UNIT ( LENGTH_MEASURE( 0.02539999999999999897 ), #6521 );
#14548=VECTOR ( 'NONE', #13861, 39.37007874015748143 ) ;
#14549=AXIS2_PLACEMENT_3D ( 'NONE', #10133, #3239, #4172 ) ;
#14556=EDGE_LOOP ( 'NONE', ( #6012, #6093 ) ) ;
#14565=ADVANCED_BREP_SHAPE_REPRESENTATION ( '', ( #10641, #8424 ), #7206 ) ;
#14566=CONICAL_SURFACE ( 'NONE', #11645, 0.3750000000000004996, 0.7853981633974536081 ) ;
#14570=EDGE_LOOP ( 'NONE', ( #12633, #11805, #9228, #6909 ) ) ;
#14581=CARTESIAN_POINT ( 'NONE',  ( 0.000000000000000000, 0.000000000000000000, 0.000000000000000000 ) ) ;
#14587=DIRECTION ( 'NONE',  ( -1.000000000000000000, -0.000000000000000000, -0.000000000000000000 ) ) ;
#14590=VERTEX_POINT ( 'NONE', #3095 ) ;
#14592=EDGE_CURVE ( 'NONE', #11914, #13586, #9457, .T. ) ;
#14593=ORIENTED_EDGE ( 'NONE', *, *, #6076, .F. ) ;
#14597=ORIENTED_EDGE ( 'NONE', *, *, #4997, .F. ) ;
#14601=ORIENTED_EDGE ( 'NONE', *, *, #5682, .T. ) ;
#14615=ORIENTED_EDGE ( 'NONE', *, *, #10727, .F. ) ;
#14616=VECTOR ( 'NONE', #11477, 39.37007874015748143 ) ;
#14625=( CONVERSION_BASED_UNIT ( 'INCH', #14540 ) LENGTH_UNIT ( ) NAMED_UNIT ( #4141 ) );
#14630=CONICAL_SURFACE ( 'NONE', #1434, 0.3750000000000004996, 0.7853981633974503884 ) ;
#14631=DIRECTION ( 'NONE',  ( 0.000000000000000000, 0.000000000000000000, 1.000000000000000000 ) ) ;
#14634=AXIS2_PLACEMENT_3D ( 'NONE', #13275, #3120, #12363 ) ;
#14636=EDGE_CURVE ( 'NONE', #4088, #9247, #5534, .T. ) ;
#14639=CARTESIAN_POINT ( 'NONE',  ( 0.06299999999999998657, 0.000000000000000000, 0.000000000000000000 ) ) ;
#14647=AXIS2_PLACEMENT_3D ( 'NONE', #9469, #11903, #3574 ) ;
#14654=EDGE_CURVE ( 'NONE', #3585, #5441, #135, .T. ) ;
#14660=CARTESIAN_POINT ( 'NONE',  ( 2.743000000000000327, 1.679378605318042395, -1.679378605318058604 ) ) ;
#14676=EDGE_LOOP ( 'NONE', ( #1337, #3283, #8608, #9100 ) ) ;
#14678=ORIENTED_EDGE ( 'NONE', *, *, #14455, .T. ) ;
#14686=DIRECTION ( 'NONE',  ( 0.000000000000000000, 0.000000000000000000, 1.000000000000000000 ) ) ;
#14699=DIRECTION ( 'NONE',  ( 1.000000000000000000, 0.000000000000000000, 0.000000000000000000 ) ) ;
#14700=EDGE_LOOP ( 'NONE', ( #13405, #12078, #14702, #4664 ) ) ;
#14702=ORIENTED_EDGE ( 'NONE', *, *, #11618, .F. ) ;
#14705=EDGE_CURVE ( 'NONE', #11506, #13193, #9526, .T. ) ;
#14710=CARTESIAN_POINT ( 'NONE',  ( 2.650000000000001688, 0.000000000000000000, 0.000000000000000000 ) ) ;
#14714=ORIENTED_EDGE ( 'NONE', *, *, #12531, .T. ) ;
#14721=DIRECTION ( 'NONE',  ( 0.000000000000000000, 0.000000000000000000, 1.000000000000000000 ) ) ;
#14722=EDGE_CURVE ( 'NONE', #2178, #13224, #8643, .T. ) ;
#14725=ORIENTED_EDGE ( 'NONE', *, *, #1631, .T. ) ;
#14726=ORIENTED_EDGE ( 'NONE', *, *, #14453, .T. ) ;
#14728=VERTEX_POINT ( 'NONE', #5768 ) ;
#14735=DIRECTION ( 'NONE',  ( -1.000000000000000000, -0.000000000000000000, -0.000000000000000000 ) ) ;
#14738=LINE ( 'NONE', #6565, #6332 ) ;
#14744=ADVANCED_FACE ( 'NONE', ( #4701 ), #7665, .F. ) ;
#14752=FACE_BOUND ( 'NONE', #7739, .T. ) ;
#14753=LINE ( 'NONE', #3282, #7461 ) ;
#14757=DIRECTION ( 'NONE',  ( 1.000000000000000000, 0.000000000000000000, 0.000000000000000000 ) ) ;
#14758=AXIS2_PLACEMENT_3D ( 'NONE', #9040, #672, #3370 ) ;
#14772=ORIENTED_EDGE ( 'NONE', *, *, #1557, .T. ) ;
#14773=CIRCLE ( 'NONE', #10630, 0.2624999999999994560 ) ;
#14776=DIRECTION ( 'NONE',  ( -1.000000000000000000, -0.000000000000000000, -0.000000000000000000 ) ) ;
#14781=VECTOR ( 'NONE', #2280, 39.37007874015748143 ) ;
#14785=VERTEX_POINT ( 'NONE', #2242 ) ;
#14787=EDGE_CURVE ( 'NONE', #969, #539, #10112, .T. ) ;
#14797=CARTESIAN_POINT ( 'NONE',  ( 2.061999999999999833, 2.257636374228145754E-16, 1.812000000000000277 ) ) ;
#14802=VERTEX_POINT ( 'NONE', #4625 ) ;
#14812=ORIENTED_EDGE ( 'NONE', *, *, #233, .F. ) ;
#14814=AXIS2_PLACEMENT_3D ( 'NONE', #10468, #7039, #2441 ) ;
#14828=DIRECTION ( 'NONE',  ( -1.000000000000000000, -0.000000000000000000, -0.000000000000000000 ) ) ;
#14833=EDGE_CURVE ( 'NONE', #13435, #5151, #3511, .T. ) ;
#14835=DIRECTION ( 'NONE',  ( 0.000000000000000000, 0.000000000000000000, -1.000000000000000000 ) ) ;
#14838=DIRECTION ( 'NONE',  ( 0.000000000000000000, 0.000000000000000000, 1.000000000000000000 ) ) ;
#14845=CARTESIAN_POINT ( 'NONE',  ( 0.6500000000000001332, 1.504103507210760471, 0.000000000000000000 ) ) ;
#14847=DIRECTION ( 'NONE',  ( 0.000000000000000000, 0.000000000000000000, -1.000000000000000000 ) ) ;
#14854=FACE_OUTER_BOUND ( 'NONE', #1174, .T. ) ;
#14856=CARTESIAN_POINT ( 'NONE',  ( 0.6500000000000001332, 0.000000000000000000, 0.000000000000000000 ) ) ;
#14859=CARTESIAN_POINT ( 'NONE',  ( 2.774999999999999911, -2.360000000000016751, -1.574999999999999956 ) ) ;
#14864=LINE ( 'NONE', #4397, #12973 ) ;
#14872=AXIS2_PLACEMENT_3D ( 'NONE', #1232, #8377, #5921 ) ;
#14876=CARTESIAN_POINT ( 'NONE',  ( 2.774999999999999911, 3.360000000000000320, -0.9800000000000012035 ) ) ;
#14877=EDGE_CURVE ( 'NONE', #1691, #13670, #3267, .T. ) ;
#14883=ORIENTED_EDGE ( 'NONE', *, *, #3764, .F. ) ;
#14899=CARTESIAN_POINT ( 'NONE',  ( 0.6180000000000012150, 0.000000000000000000, 3.000000000000000444 ) ) ;
#14903=VERTEX_POINT ( 'NONE', #2997 ) ;
#14905=CARTESIAN_POINT ( 'NONE',  ( 2.124999999999999556, -0.9799999999999436939, 3.360000000000016751 ) ) ;
#14908=EDGE_LOOP ( 'NONE', ( #4851, #13777, #2873, #11862 ) ) ;
#14912=DIRECTION ( 'NONE',  ( 0.7071067811865452413, 0.000000000000000000, -0.7071067811865497932 ) ) ;
#14915=CARTESIAN_POINT ( 'NONE',  ( 2.774999999999999911, -1.679378605318041950, 1.384878605318059064 ) ) ;
#14932=CARTESIAN_POINT ( 'NONE',  ( 2.650000000000001688, 1.224646799147353207E-16, -1.000000000000000000 ) ) ;
#14937=CIRCLE ( 'NONE', #1975, 0.7849999999999996980 ) ;
#14944=DIRECTION ( 'NONE',  ( 1.000000000000000000, 0.000000000000000000, 0.000000000000000000 ) ) ;
#14951=DIRECTION ( 'NONE',  ( -1.000000000000000000, -0.000000000000000000, -0.000000000000000000 ) ) ;
#14960=CARTESIAN_POINT ( 'NONE',  ( 2.774999999999999911, 0.000000000000000000, -1.124999999999998446 ) ) ;
#14965=CARTESIAN_POINT ( 'NONE',  ( 2.124999999999999556, 1.679378605318042395, -1.679378605318058604 ) ) ;
#14966=CIRCLE ( 'NONE', #1512, 0.2624999999999997335 ) ;
#14973=ORIENTED_EDGE ( 'NONE', *, *, #12813, .T. ) ;
#14979=EDGE_CURVE ( 'NONE', #167, #5151, #11328, .T. ) ;
#14981=DIRECTION ( 'NONE',  ( -1.000000000000000000, -0.000000000000000000, -0.000000000000000000 ) ) ;
#14986=FACE_OUTER_BOUND ( 'NONE', #7849, .T. ) ;
#14987=CARTESIAN_POINT ( 'NONE',  ( 2.774999999999999911, -1.679378605318059048, -1.679378605318041950 ) ) ;
#14989=DIRECTION ( 'NONE',  ( -1.000000000000000000, -0.000000000000000000, -0.000000000000000000 ) ) ;
#14990=AXIS2_PLACEMENT_3D ( 'NONE', #5666, #9104, #11474 ) ;
#14993=AXIS2_PLACEMENT_3D ( 'NONE', #13936, #6923, #7159 ) ;
#14996=VERTEX_POINT ( 'NONE', #9965 ) ;
#14997=ORIENTED_EDGE ( 'NONE', *, *, #3764, .T. ) ;
#15000=EDGE_CURVE ( 'NONE', #13586, #11914, #4740, .T. ) ;
#15004=AXIS2_PLACEMENT_3D ( 'NONE', #7288, #9583, #13073 ) ;
#15005=CARTESIAN_POINT ( 'NONE',  ( 2.156999999999999140, -1.679378605318041950, 1.679378605318059048 ) ) ;
#15012=DIRECTION ( 'NONE',  ( 0.7071067811865501263, 8.659560562354900811E-17, 0.7071067811865449082 ) ) ;
#15018=ADVANCED_FACE ( 'NONE', ( #13613 ), #4246, .F. ) ;
#15020=DIRECTION ( 'NONE',  ( 1.000000000000000000, 0.000000000000000000, 0.000000000000000000 ) ) ;
#15035=CARTESIAN_POINT ( 'NONE',  ( 2.156999999999999584, 1.679378605318042395, -1.679378605318058604 ) ) ;
#15062=DIRECTION ( 'NONE',  ( 0.000000000000000000, 0.000000000000000000, 1.000000000000000000 ) ) ;
#15068=DIRECTION ( 'NONE',  ( -1.000000000000000000, -0.000000000000000000, -0.000000000000000000 ) ) ;
#15074=CARTESIAN_POINT ( 'NONE',  ( 2.124999999999999556, 0.000000000000000000, 2.500000000000000444 ) ) ;
#15076=CARTESIAN_POINT ( 'NONE',  ( 0.6179999999999965521, 1.679378605318035733, -2.054378605318066153 ) ) ;
#15080=DIRECTION ( 'NONE',  ( 1.000000000000000000, 0.000000000000000000, 0.000000000000000000 ) ) ;
#15081=CIRCLE ( 'NONE', #14339, 1.125000000000000888 ) ;
#15088=ADVANCED_FACE ( 'NONE', ( #2383 ), #2299, .T. ) ;
#15093=AXIS2_PLACEMENT_3D ( 'NONE', #11966, #1394, #10519 ) ;
#15096=CARTESIAN_POINT ( 'NONE',  ( 2.774999999999999911, 2.359999999999999876, -1.575000000000016831 ) ) ;
#15101=CYLINDRICAL_SURFACE ( 'NONE', #5533, 0.2624999999999997335 ) ;
#15107=FACE_BOUND ( 'NONE', #6378, .T. ) ;
#15109=CONICAL_SURFACE ( 'NONE', #8535, 0.2944999999999998175, 0.7853981633974520538 ) ;
#15110=DIRECTION ( 'NONE',  ( -1.000000000000000000, -0.000000000000000000, -0.000000000000000000 ) ) ;
#15115=EDGE_LOOP ( 'NONE', ( #12456, #9076 ) ) ;
#15123=STYLED_ITEM('',(#15171),#10641);
#15133=ORIENTED_EDGE ( 'NONE', *, *, #11291, .T. ) ;
#15138=EDGE_LOOP ( 'NONE', ( #3674, #11215, #3993, #12264 ) ) ;
#15140=FACE_OUTER_BOUND ( 'NONE', #9387, .T. ) ;
#15144=DIRECTION ( 'NONE',  ( -1.000000000000000000, -0.000000000000000000, -0.000000000000000000 ) ) ;
#15145=DIRECTION ( 'NONE',  ( 0.000000000000000000, 0.000000000000000000, -1.000000000000000000 ) ) ;
#15146=CARTESIAN_POINT ( 'NONE',  ( 2.124999999999999556, 0.000000000000000000, 0.000000000000000000 ) ) ;
#15165=COLOUR_RGB('Dark Blue',0.08,0.2,0.34);
#15166=FILL_AREA_STYLE_COLOUR('',#15165);
#15167=FILL_AREA_STYLE('',(#15166));
#15168=SURFACE_STYLE_FILL_AREA(#15167);
#15169=SURFACE_SIDE_STYLE('',(#15168));
#15170=SURFACE_STYLE_USAGE(.BOTH.,#15169);
#15171=PRESENTATION_STYLE_ASSIGNMENT((#15170));
ENDSEC;
END-ISO-10303-21;
